ISO-10303-21;
HEADER;
/* Generated by software containing ST-Developer
 * from STEP Tools, Inc. (www.steptools.com) 
 */

FILE_DESCRIPTION(
/* description */ ('Independent AHU equipment rack. Nominal800x600 frame on1000long40squa
re aluminum posts; two removable notched shelves; welded perimeter/cro
ss rails and rear gussets; two mounting channels; four isolation pads 
and anchor-ready feet. Imported native extrusion library retained and 
cut-length parameters customized per family. Shelf hardware uses model
ed M6 rivet nuts and screws. Weld design, floor anchors and load ratin
g require engineering selection.'),
/* implementation_level */ '2;1');

FILE_NAME(
/* name */ 'Rivet nut M6.step',
/* time_stamp */ '2026-11-07T19:04:45-08:00',
/* author */ (''),
/* organization */ (''),
/* preprocessor_version */ 'ST-DEVELOPER v20.2',
/* originating_system */ 'Autodesk Translation Framework v15.17.0.0',
/* authorisation */ '');

FILE_SCHEMA (('AUTOMOTIVE_DESIGN { 1 0 10303 214 3 1 1 }'));
ENDSEC;

DATA;
#10=MECHANICAL_DESIGN_GEOMETRIC_PRESENTATION_REPRESENTATION('',(#344),#9777);
#212=B_SPLINE_SURFACE_WITH_KNOTS('',3,3,((#6744,#6745,#6746,#6747,#6748,
#6749,#6750,#6751,#6752,#6753,#6754,#6755,#6756,#6757,#6758,#6759,#6760,
#6761,#6762,#6763,#6764,#6765,#6766,#6767,#6768,#6769,#6770,#6771,#6772,
#6773,#6774,#6775,#6776,#6777,#6778,#6779,#6780,#6781,#6782,#6783,#6784,
#6785,#6786,#6787,#6788,#6789,#6790,#6791,#6792,#6793,#6794,#6795,#6796,
#6797,#6798,#6799,#6800,#6801,#6802,#6803,#6804,#6805),(#6806,#6807,#6808,
#6809,#6810,#6811,#6812,#6813,#6814,#6815,#6816,#6817,#6818,#6819,#6820,
#6821,#6822,#6823,#6824,#6825,#6826,#6827,#6828,#6829,#6830,#6831,#6832,
#6833,#6834,#6835,#6836,#6837,#6838,#6839,#6840,#6841,#6842,#6843,#6844,
#6845,#6846,#6847,#6848,#6849,#6850,#6851,#6852,#6853,#6854,#6855,#6856,
#6857,#6858,#6859,#6860,#6861,#6862,#6863,#6864,#6865,#6866,#6867),(#6868,
#6869,#6870,#6871,#6872,#6873,#6874,#6875,#6876,#6877,#6878,#6879,#6880,
#6881,#6882,#6883,#6884,#6885,#6886,#6887,#6888,#6889,#6890,#6891,#6892,
#6893,#6894,#6895,#6896,#6897,#6898,#6899,#6900,#6901,#6902,#6903,#6904,
#6905,#6906,#6907,#6908,#6909,#6910,#6911,#6912,#6913,#6914,#6915,#6916,
#6917,#6918,#6919,#6920,#6921,#6922,#6923,#6924,#6925,#6926,#6927,#6928,
#6929),(#6930,#6931,#6932,#6933,#6934,#6935,#6936,#6937,#6938,#6939,#6940,
#6941,#6942,#6943,#6944,#6945,#6946,#6947,#6948,#6949,#6950,#6951,#6952,
#6953,#6954,#6955,#6956,#6957,#6958,#6959,#6960,#6961,#6962,#6963,#6964,
#6965,#6966,#6967,#6968,#6969,#6970,#6971,#6972,#6973,#6974,#6975,#6976,
#6977,#6978,#6979,#6980,#6981,#6982,#6983,#6984,#6985,#6986,#6987,#6988,
#6989,#6990,#6991)),.UNSPECIFIED.,.F.,.F.,.F.,(4,4),(4,1,1,1,1,1,1,1,1,
1,1,1,1,1,1,1,1,1,1,1,1,1,1,1,1,1,1,1,1,1,1,1,1,1,1,1,1,1,1,1,1,1,1,1,1,
1,1,1,1,1,1,1,1,1,1,1,1,1,1,4),(0.,0.0642013499338864),(11.8589888623078,
12.8516263649797,13.8442638676517,14.8369013703236,15.8295388729956,16.8221763756675,
17.8148138783394,18.8074513810114,19.8000888836833,20.7927263863553,21.7853638890272,
22.7780013916992,23.7706388943711,24.7632763970431,25.755913899715,26.7485514023869,
27.7411889050589,28.7338264077308,29.7264639104028,30.7191014130747,31.7117389157467,
32.7043764184186,33.6970139210906,34.6896514237625,35.6822889264344,36.6749264291064,
37.6675639317783,38.6602014344503,39.6528389371222,40.6454764397942,41.6381139424661,
42.6307514451381,43.62338894781,44.6160264504819,45.6086639531539,46.6013014558258,
47.5939389584978,48.5865764611697,49.5792139638417,50.5718514665136,51.5644889691856,
52.5571264718575,53.5497639745294,54.5424014772014,55.5350389798733,56.5276764825453,
57.5203139852172,58.5129514878892,59.5055889905611,60.4982264932331,61.490863995905,
62.4835014985769,63.4761390012489,64.4687765039208,65.4614140065928,66.4540515092647,
67.4466890119367,68.4393265146086,69.4319640172805,70.4246015199525),
 .UNSPECIFIED.);
#213=B_SPLINE_SURFACE_WITH_KNOTS('',3,3,((#7196,#7197,#7198,#7199,#7200,
#7201,#7202,#7203,#7204,#7205,#7206,#7207,#7208,#7209,#7210,#7211,#7212,
#7213,#7214,#7215,#7216,#7217,#7218,#7219,#7220,#7221,#7222,#7223,#7224,
#7225,#7226,#7227,#7228,#7229,#7230,#7231,#7232,#7233,#7234,#7235,#7236,
#7237,#7238,#7239,#7240,#7241,#7242,#7243,#7244,#7245,#7246,#7247,#7248,
#7249,#7250,#7251,#7252,#7253,#7254,#7255,#7256,#7257),(#7258,#7259,#7260,
#7261,#7262,#7263,#7264,#7265,#7266,#7267,#7268,#7269,#7270,#7271,#7272,
#7273,#7274,#7275,#7276,#7277,#7278,#7279,#7280,#7281,#7282,#7283,#7284,
#7285,#7286,#7287,#7288,#7289,#7290,#7291,#7292,#7293,#7294,#7295,#7296,
#7297,#7298,#7299,#7300,#7301,#7302,#7303,#7304,#7305,#7306,#7307,#7308,
#7309,#7310,#7311,#7312,#7313,#7314,#7315,#7316,#7317,#7318,#7319),(#7320,
#7321,#7322,#7323,#7324,#7325,#7326,#7327,#7328,#7329,#7330,#7331,#7332,
#7333,#7334,#7335,#7336,#7337,#7338,#7339,#7340,#7341,#7342,#7343,#7344,
#7345,#7346,#7347,#7348,#7349,#7350,#7351,#7352,#7353,#7354,#7355,#7356,
#7357,#7358,#7359,#7360,#7361,#7362,#7363,#7364,#7365,#7366,#7367,#7368,
#7369,#7370,#7371,#7372,#7373,#7374,#7375,#7376,#7377,#7378,#7379,#7380,
#7381),(#7382,#7383,#7384,#7385,#7386,#7387,#7388,#7389,#7390,#7391,#7392,
#7393,#7394,#7395,#7396,#7397,#7398,#7399,#7400,#7401,#7402,#7403,#7404,
#7405,#7406,#7407,#7408,#7409,#7410,#7411,#7412,#7413,#7414,#7415,#7416,
#7417,#7418,#7419,#7420,#7421,#7422,#7423,#7424,#7425,#7426,#7427,#7428,
#7429,#7430,#7431,#7432,#7433,#7434,#7435,#7436,#7437,#7438,#7439,#7440,
#7441,#7442,#7443)),.UNSPECIFIED.,.F.,.F.,.F.,(4,4),(4,1,1,1,1,1,1,1,1,
1,1,1,1,1,1,1,1,1,1,1,1,1,1,1,1,1,1,1,1,1,1,1,1,1,1,1,1,1,1,1,1,1,1,1,1,
1,1,1,1,1,1,1,1,1,1,1,1,1,1,4),(0.,0.0642013499338864),(14.3984001269718,
15.3910376296438,16.3836751323157,17.3763126349876,18.3689501376596,19.3615876403315,
20.3542251430035,21.3468626456754,22.3395001483474,23.3321376510193,24.3247751536913,
25.3174126563632,26.3100501590351,27.3026876617071,28.295325164379,29.287962667051,
30.2806001697229,31.2732376723949,32.2658751750668,33.2585126777388,34.2511501804107,
35.2437876830827,36.2364251857546,37.2290626884265,38.2217001910985,39.2143376937704,
40.2069751964424,41.1996126991143,42.1922502017863,43.1848877044582,44.1775252071302,
45.1701627098021,46.162800212474,47.155437715146,48.1480752178179,49.1407127204899,
50.1333502231618,51.1259877258338,52.1186252285057,53.1112627311777,54.1039002338496,
55.0965377365215,56.0891752391935,57.0818127418654,58.0744502445374,59.0670877472093,
60.0597252498813,61.0523627525532,62.0450002552252,63.0376377578971,64.0302752605691,
65.022912763241,66.0155502659129,67.0081877685849,68.0008252712568,68.9934627739288,
69.9861002766007,70.9787377792727,71.9713752819446,72.9640127846166),
 .UNSPECIFIED.);
#216=B_SPLINE_CURVE_WITH_KNOTS('',3,(#6103,#6104,#6105,#6106,#6107,#6108,
#6109,#6110,#6111,#6112,#6113,#6114,#6115),.UNSPECIFIED.,.F.,.F.,(4,3,3,
3,4),(-3.84897440564114,-2.97791250801583,-1.98527500534389,-0.992637502671945,
0.),.UNSPECIFIED.);
#217=B_SPLINE_CURVE_WITH_KNOTS('',3,(#6118,#6119,#6120,#6121,#6122,#6123,
#6124,#6125,#6126,#6127,#6128,#6129,#6130,#6131,#6132,#6133,#6134,#6135,
#6136),.UNSPECIFIED.,.F.,.F.,(4,3,3,3,3,3,4),(2.01694489302846,2.97791250801583,
3.97055001068778,4.96318751335972,5.95582501603167,6.94846251870361,7.59274844815667),
 .UNSPECIFIED.);
#218=B_SPLINE_CURVE_WITH_KNOTS('',3,(#6141,#6142,#6143,#6144,#6145,#6146,
#6147,#6148,#6149,#6150,#6151,#6152,#6153,#6154,#6155,#6156,#6157,#6158,
#6159,#6160,#6161,#6162,#6163,#6164,#6165),.UNSPECIFIED.,.F.,.F.,(4,3,3,
3,3,3,3,3,4),(-10.1321597128207,-9.92637502671944,-8.9337375240475,-7.94110002137556,
-6.94846251870361,-5.95582501603167,-4.96318751335972,-3.97055001068778,
-3.84897440564114),.UNSPECIFIED.);
#219=B_SPLINE_CURVE_WITH_KNOTS('',3,(#6166,#6167,#6168,#6169,#6170,#6171,
#6172,#6173,#6174,#6175,#6176,#6177,#6178,#6179,#6180,#6181,#6182,#6183,
#6184,#6185,#6186,#6187),.UNSPECIFIED.,.F.,.F.,(4,3,3,3,3,3,3,4),(7.59274844815667,
7.94110002137556,8.9337375240475,9.92637502671945,10.9190125293914,11.9116500320633,
12.9042875347353,13.8759337553363),.UNSPECIFIED.);
#220=B_SPLINE_CURVE_WITH_KNOTS('',3,(#6192,#6193,#6194,#6195,#6196,#6197,
#6198,#6199,#6200,#6201,#6202,#6203,#6204,#6205,#6206,#6207,#6208,#6209,
#6210,#6211,#6212,#6213),.UNSPECIFIED.,.F.,.F.,(4,3,3,3,3,3,3,4),(-16.4153450200003,
-15.8822000427511,-14.8895625400792,-13.8969250374072,-12.9042875347353,
-11.9116500320633,-10.9190125293914,-10.1321597128207),.UNSPECIFIED.);
#221=B_SPLINE_CURVE_WITH_KNOTS('',3,(#6214,#6215,#6216,#6217,#6218,#6219,
#6220,#6221,#6222,#6223,#6224,#6225,#6226,#6227,#6228,#6229,#6230,#6231,
#6232,#6233,#6234,#6235,#6236,#6237,#6238),.UNSPECIFIED.,.F.,.F.,(4,3,3,
3,3,3,3,3,4),(13.8759337553363,13.8969250374072,14.8895625400792,15.8822000427511,
16.8748375454231,17.867475048095,18.860112550767,19.8527500534389,20.1591190625158),
 .UNSPECIFIED.);
#222=B_SPLINE_CURVE_WITH_KNOTS('',3,(#6243,#6244,#6245,#6246,#6247,#6248,
#6249,#6250,#6251,#6252,#6253,#6254,#6255,#6256,#6257,#6258,#6259,#6260,
#6261,#6262,#6263,#6264),.UNSPECIFIED.,.F.,.F.,(4,3,3,3,3,3,3,4),(-22.6985303271799,
-21.8380250587828,-20.8453875561108,-19.8527500534389,-18.8601125507669,
-17.867475048095,-16.8748375454231,-16.4153450200003),.UNSPECIFIED.);
#223=B_SPLINE_CURVE_WITH_KNOTS('',3,(#6265,#6266,#6267,#6268,#6269,#6270,
#6271,#6272,#6273,#6274,#6275,#6276,#6277,#6278,#6279,#6280,#6281,#6282,
#6283,#6284,#6285,#6286),.UNSPECIFIED.,.F.,.F.,(4,3,3,3,3,3,3,4),(20.1591190625158,
20.8453875561109,21.8380250587828,22.8306625614547,23.8233000641267,24.8159375667986,
25.8085750694706,26.4423043696954),.UNSPECIFIED.);
#224=B_SPLINE_CURVE_WITH_KNOTS('',3,(#6291,#6292,#6293,#6294,#6295,#6296,
#6297,#6298,#6299,#6300,#6301,#6302,#6303,#6304,#6305,#6306,#6307,#6308,
#6309,#6310,#6311,#6312,#6313,#6314,#6315),.UNSPECIFIED.,.F.,.F.,(4,3,3,
3,3,3,3,3,4),(-28.9817156343595,-28.7864875774864,-27.7938500748144,-26.8012125721425,
-25.8085750694705,-24.8159375667986,-23.8233000641267,-22.8306625614547,
-22.6985303271799),.UNSPECIFIED.);
#225=B_SPLINE_CURVE_WITH_KNOTS('',3,(#6316,#6317,#6318,#6319,#6320,#6321,
#6322,#6323,#6324,#6325,#6326,#6327,#6328,#6329,#6330,#6331,#6332,#6333,
#6334,#6335,#6336,#6337),.UNSPECIFIED.,.F.,.F.,(4,3,3,3,3,3,3,4),(26.4423043696954,
26.8012125721425,27.7938500748145,28.7864875774864,29.7791250801584,30.7717625828303,
31.7644000855022,32.725489676875),.UNSPECIFIED.);
#226=B_SPLINE_CURVE_WITH_KNOTS('',3,(#6342,#6343,#6344,#6345,#6346,#6347,
#6348,#6349,#6350,#6351,#6352,#6353,#6354,#6355,#6356,#6357,#6358,#6359,
#6360,#6361,#6362,#6363),.UNSPECIFIED.,.F.,.F.,(4,3,3,3,3,3,3,4),(-35.2649009415391,
-34.7423125935181,-33.7496750908461,-32.7570375881742,-31.7644000855022,
-30.7717625828303,-29.7791250801583,-28.9817156343595),.UNSPECIFIED.);
#227=B_SPLINE_CURVE_WITH_KNOTS('',3,(#6364,#6365,#6366,#6367,#6368,#6369,
#6370,#6371,#6372,#6373,#6374,#6375,#6376,#6377,#6378,#6379,#6380,#6381,
#6382,#6383,#6384,#6385,#6386,#6387,#6388),.UNSPECIFIED.,.F.,.F.,(4,3,3,
3,3,3,3,3,4),(32.725489676875,32.7570375881742,33.7496750908461,34.7423125935181,
35.73495009619,36.727587598862,37.7202251015339,38.7128626042059,39.0086749840546),
 .UNSPECIFIED.);
#228=B_SPLINE_CURVE_WITH_KNOTS('',3,(#6393,#6394,#6395,#6396,#6397,#6398,
#6399,#6400,#6401,#6402,#6403,#6404,#6405,#6406,#6407,#6408,#6409,#6410,
#6411,#6412,#6413,#6414),.UNSPECIFIED.,.F.,.F.,(4,3,3,3,3,3,3,4),(-41.5480862487187,
-40.6981376095497,-39.7055001068778,-38.7128626042058,-37.7202251015339,
-36.7275875988619,-35.73495009619,-35.2649009415391),.UNSPECIFIED.);
#229=B_SPLINE_CURVE_WITH_KNOTS('',3,(#6415,#6416,#6417,#6418,#6419,#6420,
#6421,#6422,#6423,#6424,#6425,#6426,#6427,#6428,#6429,#6430,#6431,#6432,
#6433,#6434,#6435,#6436),.UNSPECIFIED.,.F.,.F.,(4,3,3,3,3,3,3,4),(39.0086749840546,
39.7055001068778,40.6981376095497,41.6907751122217,42.6834126148936,43.6760501175656,
44.6686876202375,45.2918602912342),.UNSPECIFIED.);
#230=B_SPLINE_CURVE_WITH_KNOTS('',3,(#6441,#6442,#6443,#6444,#6445,#6446,
#6447,#6448,#6449,#6450,#6451,#6452,#6453,#6454,#6455,#6456,#6457,#6458,
#6459,#6460,#6461,#6462,#6463,#6464,#6465),.UNSPECIFIED.,.F.,.F.,(4,3,3,
3,3,3,3,3,4),(-47.8312715558982,-47.6466001282533,-46.6539626255814,-45.6613251229094,
-44.6686876202375,-43.6760501175656,-42.6834126148936,-41.6907751122217,
-41.5480862487187),.UNSPECIFIED.);
#231=B_SPLINE_CURVE_WITH_KNOTS('',3,(#6466,#6467,#6468,#6469,#6470,#6471,
#6472,#6473,#6474,#6475,#6476,#6477,#6478,#6479,#6480,#6481,#6482,#6483,
#6484,#6485,#6486,#6487),.UNSPECIFIED.,.F.,.F.,(4,3,3,3,3,3,3,4),(45.2918602912342,
45.6613251229095,46.6539626255814,47.6466001282534,48.6392376309253,49.6318751335972,
50.6245126362692,51.5750455984138),.UNSPECIFIED.);
#232=B_SPLINE_CURVE_WITH_KNOTS('',3,(#6493,#6494,#6495,#6496),
 .UNSPECIFIED.,.F.,.F.,(4,4),(57.8582309055934,58.5656126576447),
 .UNSPECIFIED.);
#233=B_SPLINE_CURVE_WITH_KNOTS('',3,(#6499,#6500,#6501,#6502,#6503,#6504,
#6505,#6506,#6507,#6508),.UNSPECIFIED.,.F.,.F.,(4,3,3,4),(-56.5486677646163,
-55.5877001496289,-54.5950626469569,-54.1144568630778),.UNSPECIFIED.);
#234=B_SPLINE_CURVE_WITH_KNOTS('',3,(#6514,#6515,#6516,#6517,#6518,#6519,
#6520,#6521),.UNSPECIFIED.,.F.,.F.,(4,1,1,1,1,4),(65.9734457253856,66.4540515092647,
67.4466890119367,68.4393265146086,69.4319640172805,70.4246015199525),
 .UNSPECIFIED.);
#235=B_SPLINE_CURVE_WITH_KNOTS('',3,(#6524,#6525,#6526,#6527,#6528,#6529,
#6530,#6531,#6532),.UNSPECIFIED.,.F.,.F.,(4,1,1,1,1,1,4),(65.9734457253856,
66.0155502659129,67.0081877685849,68.0008252712568,68.9934627739288,69.9861002766007,
70.9470678915881),.UNSPECIFIED.);
#236=B_SPLINE_CURVE_WITH_KNOTS('',3,(#6537,#6538,#6539,#6540,#6541,#6542,
#6543,#6544,#6545,#6546),.UNSPECIFIED.,.F.,.F.,(4,1,1,1,1,1,1,4),(59.6902604182061,
60.4982264932331,61.490863995905,62.4835014985769,63.4761390012489,64.4687765039208,
65.4614140065928,65.9734457253856),.UNSPECIFIED.);
#237=B_SPLINE_CURVE_WITH_KNOTS('',3,(#6547,#6548,#6549,#6550,#6551,#6552,
#6553,#6554,#6555,#6556),.UNSPECIFIED.,.F.,.F.,(4,1,1,1,1,1,1,4),(59.6902604182061,
60.0597252498813,61.0523627525532,62.0450002552252,63.0376377578971,64.0302752605691,
65.022912763241,65.9734457253856),.UNSPECIFIED.);
#238=B_SPLINE_CURVE_WITH_KNOTS('',3,(#6561,#6562,#6563,#6564,#6565,#6566,
#6567,#6568,#6569,#6570,#6571),.UNSPECIFIED.,.F.,.F.,(4,1,1,1,1,1,1,1,4),
(53.4070751110265,53.5497639745294,54.5424014772014,55.5350389798733,56.5276764825453,
57.5203139852172,58.5129514878892,59.5055889905611,59.6902604182061),
 .UNSPECIFIED.);
#239=B_SPLINE_CURVE_WITH_KNOTS('',3,(#6572,#6573,#6574,#6575,#6576,#6577,
#6578,#6579,#6580,#6581),.UNSPECIFIED.,.F.,.F.,(4,1,1,1,1,1,1,4),(53.4070751110265,
54.1039002338496,55.0965377365215,56.0891752391935,57.0818127418654,58.0744502445374,
59.0670877472093,59.6902604182061),.UNSPECIFIED.);
#240=B_SPLINE_CURVE_WITH_KNOTS('',3,(#6586,#6587,#6588,#6589,#6590,#6591,
#6592,#6593,#6594,#6595),.UNSPECIFIED.,.F.,.F.,(4,1,1,1,1,1,1,4),(47.1238898038469,
47.5939389584978,48.5865764611697,49.5792139638417,50.5718514665136,51.5644889691856,
52.5571264718575,53.4070751110265),.UNSPECIFIED.);
#241=B_SPLINE_CURVE_WITH_KNOTS('',3,(#6596,#6597,#6598,#6599,#6600,#6601,
#6602,#6603,#6604,#6605,#6606),.UNSPECIFIED.,.F.,.F.,(4,1,1,1,1,1,1,1,4),
(47.1238898038469,47.155437715146,48.1480752178179,49.1407127204899,50.1333502231618,
51.1259877258338,52.1186252285057,53.1112627311777,53.4070751110265),
 .UNSPECIFIED.);
#242=B_SPLINE_CURVE_WITH_KNOTS('',3,(#6611,#6612,#6613,#6614,#6615,#6616,
#6617,#6618,#6619,#6620),.UNSPECIFIED.,.F.,.F.,(4,1,1,1,1,1,1,4),(40.8407044966673,
41.6381139424661,42.6307514451381,43.62338894781,44.6160264504819,45.6086639531539,
46.6013014558258,47.1238898038469),.UNSPECIFIED.);
#243=B_SPLINE_CURVE_WITH_KNOTS('',3,(#6621,#6622,#6623,#6624,#6625,#6626,
#6627,#6628,#6629,#6630),.UNSPECIFIED.,.F.,.F.,(4,1,1,1,1,1,1,4),(40.8407044966673,
41.1996126991143,42.1922502017863,43.1848877044582,44.1775252071302,45.1701627098021,
46.162800212474,47.1238898038469),.UNSPECIFIED.);
#244=B_SPLINE_CURVE_WITH_KNOTS('',3,(#6635,#6636,#6637,#6638,#6639,#6640,
#6641,#6642,#6643,#6644,#6645),.UNSPECIFIED.,.F.,.F.,(4,1,1,1,1,1,1,1,4),
(34.5575191894877,34.6896514237625,35.6822889264344,36.6749264291064,37.6675639317783,
38.6602014344503,39.6528389371222,40.6454764397942,40.8407044966673),
 .UNSPECIFIED.);
#245=B_SPLINE_CURVE_WITH_KNOTS('',3,(#6646,#6647,#6648,#6649,#6650,#6651,
#6652,#6653,#6654,#6655),.UNSPECIFIED.,.F.,.F.,(4,1,1,1,1,1,1,4),(34.5575191894877,
35.2437876830827,36.2364251857546,37.2290626884265,38.2217001910985,39.2143376937704,
40.2069751964424,40.8407044966673),.UNSPECIFIED.);
#246=B_SPLINE_CURVE_WITH_KNOTS('',3,(#6660,#6661,#6662,#6663,#6664,#6665,
#6666,#6667,#6668,#6669),.UNSPECIFIED.,.F.,.F.,(4,1,1,1,1,1,1,4),(28.2743338823081,
28.7338264077308,29.7264639104028,30.7191014130747,31.7117389157467,32.7043764184186,
33.6970139210906,34.5575191894877),.UNSPECIFIED.);
#247=B_SPLINE_CURVE_WITH_KNOTS('',3,(#6670,#6671,#6672,#6673,#6674,#6675,
#6676,#6677,#6678,#6679,#6680),.UNSPECIFIED.,.F.,.F.,(4,1,1,1,1,1,1,1,4),
(28.2743338823081,28.295325164379,29.287962667051,30.2806001697229,31.2732376723949,
32.2658751750668,33.2585126777388,34.2511501804107,34.5575191894877),
 .UNSPECIFIED.);
#248=B_SPLINE_CURVE_WITH_KNOTS('',3,(#6685,#6686,#6687,#6688,#6689,#6690,
#6691,#6692,#6693,#6694),.UNSPECIFIED.,.F.,.F.,(4,1,1,1,1,1,1,4),(21.9911485751285,
22.7780013916992,23.7706388943711,24.7632763970431,25.755913899715,26.7485514023869,
27.7411889050589,28.2743338823081),.UNSPECIFIED.);
#249=B_SPLINE_CURVE_WITH_KNOTS('',3,(#6695,#6696,#6697,#6698,#6699,#6700,
#6701,#6702,#6703,#6704),.UNSPECIFIED.,.F.,.F.,(4,1,1,1,1,1,1,4),(21.9911485751285,
22.3395001483474,23.3321376510193,24.3247751536913,25.3174126563632,26.3100501590351,
27.3026876617071,28.2743338823081),.UNSPECIFIED.);
#250=B_SPLINE_CURVE_WITH_KNOTS('',3,(#6710,#6711,#6712,#6713,#6714),
 .UNSPECIFIED.,.F.,.F.,(4,1,4),(14.3984001269718,15.3910376296438,15.7079632679489),
 .UNSPECIFIED.);
#251=B_SPLINE_CURVE_WITH_KNOTS('',3,(#6717,#6718,#6719,#6720,#6721),
 .UNSPECIFIED.,.F.,.F.,(4,1,4),(13.8759337553362,14.8369013703236,15.7079632679489),
 .UNSPECIFIED.);
#252=B_SPLINE_CURVE_WITH_KNOTS('',3,(#6723,#6724,#6725,#6726,#6727,#6728,
#6729,#6730,#6731,#6732,#6733),.UNSPECIFIED.,.F.,.F.,(4,1,1,1,1,1,1,1,4),
(15.7079632679489,15.8295388729956,16.8221763756675,17.8148138783394,18.8074513810114,
19.8000888836833,20.7927263863553,21.7853638890272,21.9911485751285),
 .UNSPECIFIED.);
#253=B_SPLINE_CURVE_WITH_KNOTS('',3,(#6734,#6735,#6736,#6737,#6738,#6739,
#6740,#6741,#6742,#6743),.UNSPECIFIED.,.F.,.F.,(4,1,1,1,1,1,1,4),(15.7079632679489,
16.3836751323157,17.3763126349876,18.3689501376596,19.3615876403315,20.3542251430035,
21.3468626456754,21.9911485751285),.UNSPECIFIED.);
#254=B_SPLINE_CURVE_WITH_KNOTS('',3,(#6992,#6993,#6994,#6995,#6996,#6997,
#6998,#6999,#7000,#7001,#7002,#7003,#7004,#7005,#7006,#7007,#7008,#7009,
#7010,#7011,#7012,#7013,#7014,#7015,#7016,#7017,#7018,#7019,#7020,#7021,
#7022,#7023,#7024,#7025,#7026,#7027,#7028,#7029,#7030,#7031,#7032,#7033,
#7034,#7035,#7036,#7037,#7038,#7039,#7040,#7041,#7042,#7043,#7044,#7045,
#7046,#7047,#7048,#7049,#7050,#7051,#7052,#7053,#7054,#7055,#7056,#7057,
#7058,#7059,#7060,#7061,#7062,#7063,#7064,#7065,#7066,#7067,#7068,#7069,
#7070,#7071,#7072,#7073,#7074,#7075,#7076,#7077,#7078,#7079,#7080,#7081,
#7082),.UNSPECIFIED.,.F.,.F.,(4,3,3,3,3,3,3,3,3,3,3,3,3,3,3,3,3,3,3,3,3,
3,3,3,3,3,3,3,3,3,4),(0.,0.0297334041407413,0.060121188705027,0.0893594248720358,
0.114942881518169,0.12062818802643,0.150387503639245,0.17998043773465,0.208492097811262,
0.220468872654926,0.228874065707467,0.234174696232567,0.264100887136832,
0.292003393472183,0.294027078041098,0.3229737914971,0.339361239182251,0.343534194645605,
0.371627921656661,0.399766246005302,0.427498548100254,0.437962627154652,
0.445613074679864,0.450368652920306,0.478071944275567,0.498849412792013,
0.508237562401581,0.513366228472013,0.539276359085418,0.561181818341351,
0.569248610399392),.UNSPECIFIED.);
#255=B_SPLINE_CURVE_WITH_KNOTS('',3,(#7083,#7084,#7085,#7086,#7087,#7088,
#7089,#7090,#7091,#7092,#7093,#7094,#7095,#7096,#7097,#7098,#7099,#7100,
#7101,#7102,#7103,#7104,#7105,#7106,#7107,#7108,#7109,#7110,#7111,#7112,
#7113,#7114,#7115,#7116,#7117,#7118,#7119,#7120,#7121,#7122,#7123,#7124,
#7125,#7126,#7127,#7128,#7129,#7130,#7131,#7132,#7133,#7134,#7135,#7136,
#7137,#7138,#7139,#7140,#7141,#7142,#7143,#7144,#7145,#7146,#7147,#7148,
#7149,#7150,#7151,#7152,#7153,#7154,#7155,#7156,#7157,#7158,#7159,#7160,
#7161,#7162,#7163,#7164,#7165,#7166,#7167,#7168,#7169,#7170,#7171,#7172,
#7173),.UNSPECIFIED.,.F.,.F.,(4,3,3,3,3,3,3,3,3,3,3,3,3,3,3,3,3,3,3,3,3,
3,3,3,3,3,3,3,3,3,4),(0.,0.0253741918154253,0.0514188574543204,0.0781724584567371,
0.0899216140471938,0.0966260843074363,0.102679517247254,0.129987895141776,
0.157743514226617,0.184669552038376,0.1959299763122,0.202971688416046,0.207100127397784,
0.236273896435719,0.265447665473654,0.293335582735069,0.30266718021653,
0.30870328948035,0.314529473155204,0.342600363170572,0.371717504292952,
0.401165116978085,0.421327065973589,0.426436909350868,0.456483211929156,
0.481642425143559,0.494284407148645,0.499857105743045,0.530355157019413,
0.557120064786768,0.566847306048084),.UNSPECIFIED.);
#256=B_SPLINE_CURVE_WITH_KNOTS('',3,(#7174,#7175,#7176,#7177,#7178,#7179,
#7180,#7181,#7182,#7183,#7184,#7185,#7186,#7187,#7188,#7189,#7190,#7191,
#7192,#7193,#7194,#7195),.UNSPECIFIED.,.F.,.F.,(4,3,3,3,3,3,3,4),(-54.1144568630778,
-53.602425144285,-52.609787641613,-51.6171501389411,-50.6245126362692,-49.6318751335972,
-48.6392376309253,-47.8312715558982),.UNSPECIFIED.);
#257=B_SPLINE_CURVE_WITH_KNOTS('',3,(#7444,#7445,#7446,#7447,#7448,#7449,
#7450,#7451,#7452,#7453,#7454,#7455,#7456,#7457,#7458,#7459,#7460,#7461,
#7462,#7463,#7464,#7465,#7466,#7467,#7468,#7469,#7470,#7471,#7472,#7473,
#7474,#7475,#7476,#7477,#7478,#7479,#7480,#7481,#7482,#7483,#7484,#7485,
#7486,#7487,#7488,#7489,#7490,#7491,#7492,#7493,#7494,#7495,#7496,#7497,
#7498,#7499,#7500,#7501,#7502,#7503,#7504,#7505,#7506,#7507,#7508,#7509,
#7510,#7511,#7512,#7513,#7514,#7515,#7516,#7517,#7518,#7519,#7520,#7521,
#7522,#7523,#7524,#7525,#7526,#7527,#7528,#7529,#7530,#7531,#7532,#7533,
#7534),.UNSPECIFIED.,.F.,.F.,(4,3,3,3,3,3,3,3,3,3,3,3,3,3,3,3,3,3,3,3,3,
3,3,3,3,3,3,3,3,3,4),(0.,0.0253741449502821,0.0514187685629996,0.0781723806768318,
0.0899215962667811,0.0966260820429981,0.10267951725872,0.129987863111654,
0.157743467348106,0.184669516879494,0.195929969047891,0.202971685861533,
0.207100122286109,0.236273893879883,0.265447665473657,0.293335606992279,
0.302667231074582,0.30870349429627,0.314529468018238,0.342600392862402,
0.371717549581951,0.401165166107868,0.421327178828175,0.42643689855922,
0.456483208176513,0.481642422329078,0.494284406072129,0.499857109233687,
0.530355160772762,0.557120064786773,0.566847306048096),.UNSPECIFIED.);
#258=B_SPLINE_CURVE_WITH_KNOTS('',3,(#7535,#7536,#7537,#7538,#7539,#7540,
#7541,#7542,#7543,#7544,#7545,#7546,#7547,#7548,#7549,#7550,#7551,#7552,
#7553,#7554,#7555,#7556,#7557,#7558,#7559),.UNSPECIFIED.,.F.,.F.,(4,3,3,
3,3,3,3,3,4),(51.5750455984138,51.6171501389411,52.6097876416131,53.602425144285,
54.595062646957,55.5877001496289,56.5803376523009,57.5729751549728,57.8582309055934),
 .UNSPECIFIED.);
#259=B_SPLINE_CURVE_WITH_KNOTS('',3,(#7560,#7561,#7562,#7563,#7564,#7565,
#7566,#7567,#7568,#7569,#7570,#7571,#7572,#7573,#7574,#7575,#7576,#7577,
#7578,#7579,#7580,#7581,#7582,#7583,#7584,#7585,#7586,#7587,#7588,#7589,
#7590,#7591,#7592,#7593,#7594,#7595,#7596,#7597,#7598,#7599,#7600,#7601,
#7602,#7603,#7604,#7605,#7606,#7607,#7608,#7609,#7610,#7611,#7612,#7613,
#7614,#7615,#7616,#7617,#7618,#7619,#7620,#7621,#7622,#7623,#7624,#7625,
#7626,#7627,#7628,#7629,#7630,#7631,#7632,#7633,#7634,#7635,#7636,#7637,
#7638,#7639,#7640,#7641,#7642,#7643,#7644,#7645,#7646,#7647,#7648,#7649,
#7650),.UNSPECIFIED.,.F.,.F.,(4,3,3,3,3,3,3,3,3,3,3,3,3,3,3,3,3,3,3,3,3,
3,3,3,3,3,3,3,3,3,4),(0.,0.0297333652245644,0.0601211311135188,0.0893593744794667,
0.114942837424671,0.120628184894895,0.150387501019274,0.179980446751773,
0.208492104574105,0.220468888246807,0.228874110566872,0.234174709732106,
0.264100893886604,0.292003410907553,0.294027078041101,0.322973790194836,
0.339361247095814,0.343534203933017,0.371627930217731,0.399766255738478,
0.427498569351598,0.437962674970173,0.44561323665522,0.450368688624651,
0.478071971053836,0.498849432875724,0.508237633125922,0.51336624635807,
0.539276402540273,0.561181818341388,0.569248610399427),.UNSPECIFIED.);
#322=SHAPE_REPRESENTATION_RELATIONSHIP('SRR','None',#9866,#333);
#333=ADVANCED_BREP_SHAPE_REPRESENTATION('',(#355),#9775);
#344=STYLED_ITEM('',(#9929),#355);
#355=MANIFOLD_SOLID_BREP('Body1',#3849);
#403=FACE_BOUND('',#897,.T.);
#404=FACE_BOUND('',#899,.T.);
#405=FACE_BOUND('',#901,.T.);
#406=FACE_BOUND('',#905,.T.);
#407=FACE_BOUND('',#910,.T.);
#487=PLANE('',#4240);
#488=PLANE('',#4242);
#489=PLANE('',#4245);
#490=PLANE('',#4251);
#491=PLANE('',#4257);
#631=FACE_OUTER_BOUND('',#875,.T.);
#632=FACE_OUTER_BOUND('',#876,.T.);
#633=FACE_OUTER_BOUND('',#877,.T.);
#634=FACE_OUTER_BOUND('',#878,.T.);
#635=FACE_OUTER_BOUND('',#879,.T.);
#636=FACE_OUTER_BOUND('',#880,.T.);
#637=FACE_OUTER_BOUND('',#881,.T.);
#638=FACE_OUTER_BOUND('',#882,.T.);
#639=FACE_OUTER_BOUND('',#883,.T.);
#640=FACE_OUTER_BOUND('',#884,.T.);
#641=FACE_OUTER_BOUND('',#885,.T.);
#642=FACE_OUTER_BOUND('',#886,.T.);
#643=FACE_OUTER_BOUND('',#887,.T.);
#644=FACE_OUTER_BOUND('',#888,.T.);
#645=FACE_OUTER_BOUND('',#889,.T.);
#646=FACE_OUTER_BOUND('',#890,.T.);
#647=FACE_OUTER_BOUND('',#891,.T.);
#648=FACE_OUTER_BOUND('',#892,.T.);
#649=FACE_OUTER_BOUND('',#893,.T.);
#650=FACE_OUTER_BOUND('',#894,.T.);
#651=FACE_OUTER_BOUND('',#895,.T.);
#652=FACE_OUTER_BOUND('',#896,.T.);
#653=FACE_OUTER_BOUND('',#898,.T.);
#654=FACE_OUTER_BOUND('',#900,.T.);
#655=FACE_OUTER_BOUND('',#902,.T.);
#656=FACE_OUTER_BOUND('',#903,.T.);
#657=FACE_OUTER_BOUND('',#904,.T.);
#658=FACE_OUTER_BOUND('',#906,.T.);
#659=FACE_OUTER_BOUND('',#907,.T.);
#660=FACE_OUTER_BOUND('',#908,.T.);
#661=FACE_OUTER_BOUND('',#909,.T.);
#875=EDGE_LOOP('',(#3181,#3182,#3183,#3184));
#876=EDGE_LOOP('',(#3185,#3186,#3187,#3188));
#877=EDGE_LOOP('',(#3189,#3190,#3191,#3192));
#878=EDGE_LOOP('',(#3193,#3194,#3195,#3196));
#879=EDGE_LOOP('',(#3197,#3198,#3199,#3200));
#880=EDGE_LOOP('',(#3201,#3202,#3203,#3204));
#881=EDGE_LOOP('',(#3205,#3206,#3207,#3208));
#882=EDGE_LOOP('',(#3209,#3210,#3211,#3212));
#883=EDGE_LOOP('',(#3213,#3214,#3215,#3216));
#884=EDGE_LOOP('',(#3217,#3218,#3219,#3220));
#885=EDGE_LOOP('',(#3221,#3222,#3223,#3224));
#886=EDGE_LOOP('',(#3225,#3226,#3227,#3228));
#887=EDGE_LOOP('',(#3229,#3230,#3231,#3232));
#888=EDGE_LOOP('',(#3233,#3234,#3235,#3236));
#889=EDGE_LOOP('',(#3237,#3238,#3239,#3240));
#890=EDGE_LOOP('',(#3241,#3242,#3243,#3244));
#891=EDGE_LOOP('',(#3245,#3246,#3247,#3248));
#892=EDGE_LOOP('',(#3249,#3250,#3251,#3252));
#893=EDGE_LOOP('',(#3253,#3254,#3255,#3256));
#894=EDGE_LOOP('',(#3257,#3258,#3259,#3260,#3261,#3262,#3263,#3264,#3265,
#3266,#3267,#3268,#3269,#3270,#3271,#3272,#3273,#3274,#3275,#3276,#3277,
#3278));
#895=EDGE_LOOP('',(#3279,#3280,#3281,#3282,#3283,#3284,#3285,#3286,#3287,
#3288,#3289,#3290,#3291,#3292,#3293,#3294,#3295,#3296,#3297,#3298,#3299,
#3300));
#896=EDGE_LOOP('',(#3301));
#897=EDGE_LOOP('',(#3302,#3303,#3304,#3305));
#898=EDGE_LOOP('',(#3306));
#899=EDGE_LOOP('',(#3307));
#900=EDGE_LOOP('',(#3308));
#901=EDGE_LOOP('',(#3309));
#902=EDGE_LOOP('',(#3310,#3311,#3312,#3313));
#903=EDGE_LOOP('',(#3314,#3315,#3316,#3317));
#904=EDGE_LOOP('',(#3318));
#905=EDGE_LOOP('',(#3319));
#906=EDGE_LOOP('',(#3320,#3321,#3322,#3323));
#907=EDGE_LOOP('',(#3324,#3325,#3326,#3327));
#908=EDGE_LOOP('',(#3328,#3329,#3330,#3331));
#909=EDGE_LOOP('',(#3332));
#910=EDGE_LOOP('',(#3333,#3334,#3335,#3336));
#1180=LINE('',#6101,#1473);
#1181=LINE('',#6140,#1474);
#1182=LINE('',#6191,#1475);
#1183=LINE('',#6242,#1476);
#1184=LINE('',#6290,#1477);
#1185=LINE('',#6341,#1478);
#1186=LINE('',#6392,#1479);
#1187=LINE('',#6440,#1480);
#1188=LINE('',#6491,#1481);
#1189=LINE('',#6512,#1482);
#1190=LINE('',#6536,#1483);
#1191=LINE('',#6560,#1484);
#1192=LINE('',#6585,#1485);
#1193=LINE('',#6610,#1486);
#1194=LINE('',#6634,#1487);
#1195=LINE('',#6659,#1488);
#1196=LINE('',#6684,#1489);
#1197=LINE('',#6708,#1490);
#1198=LINE('',#7665,#1491);
#1199=LINE('',#7668,#1492);
#1200=LINE('',#7676,#1493);
#1201=LINE('',#7679,#1494);
#1473=VECTOR('',#5071,3.);
#1474=VECTOR('',#5076,3.);
#1475=VECTOR('',#5079,3.);
#1476=VECTOR('',#5082,3.);
#1477=VECTOR('',#5085,3.);
#1478=VECTOR('',#5088,3.);
#1479=VECTOR('',#5091,3.);
#1480=VECTOR('',#5094,3.);
#1481=VECTOR('',#5097,3.);
#1482=VECTOR('',#5102,3.0735);
#1483=VECTOR('',#5107,3.0735);
#1484=VECTOR('',#5110,3.0735);
#1485=VECTOR('',#5113,3.0735);
#1486=VECTOR('',#5116,3.0735);
#1487=VECTOR('',#5119,3.0735);
#1488=VECTOR('',#5122,3.0735);
#1489=VECTOR('',#5125,3.0735);
#1490=VECTOR('',#5128,3.0735);
#1491=VECTOR('',#5151,7.);
#1492=VECTOR('',#5154,5.);
#1493=VECTOR('',#5165,7.);
#1494=VECTOR('',#5170,5.);
#1641=CIRCLE('',#4218,2.5175);
#1642=CIRCLE('',#4227,2.5175);
#1643=CIRCLE('',#4229,3.0735);
#1644=CIRCLE('',#4238,3.0735);
#1645=CIRCLE('',#4241,7.);
#1646=CIRCLE('',#4243,7.);
#1647=CIRCLE('',#4244,5.);
#1648=CIRCLE('',#4246,7.);
#1649=CIRCLE('',#4247,5.);
#1650=CIRCLE('',#4250,5.);
#1651=CIRCLE('',#4252,7.);
#1652=CIRCLE('',#4253,5.);
#1882=VERTEX_POINT('',#6099);
#1883=VERTEX_POINT('',#6100);
#1884=VERTEX_POINT('',#6102);
#1885=VERTEX_POINT('',#6116);
#1886=VERTEX_POINT('',#6138);
#1887=VERTEX_POINT('',#6139);
#1888=VERTEX_POINT('',#6189);
#1889=VERTEX_POINT('',#6190);
#1890=VERTEX_POINT('',#6240);
#1891=VERTEX_POINT('',#6241);
#1892=VERTEX_POINT('',#6288);
#1893=VERTEX_POINT('',#6289);
#1894=VERTEX_POINT('',#6339);
#1895=VERTEX_POINT('',#6340);
#1896=VERTEX_POINT('',#6390);
#1897=VERTEX_POINT('',#6391);
#1898=VERTEX_POINT('',#6438);
#1899=VERTEX_POINT('',#6439);
#1900=VERTEX_POINT('',#6489);
#1901=VERTEX_POINT('',#6490);
#1902=VERTEX_POINT('',#6492);
#1903=VERTEX_POINT('',#6497);
#1904=VERTEX_POINT('',#6510);
#1905=VERTEX_POINT('',#6511);
#1906=VERTEX_POINT('',#6513);
#1907=VERTEX_POINT('',#6522);
#1908=VERTEX_POINT('',#6534);
#1909=VERTEX_POINT('',#6535);
#1910=VERTEX_POINT('',#6558);
#1911=VERTEX_POINT('',#6559);
#1912=VERTEX_POINT('',#6583);
#1913=VERTEX_POINT('',#6584);
#1914=VERTEX_POINT('',#6608);
#1915=VERTEX_POINT('',#6609);
#1916=VERTEX_POINT('',#6632);
#1917=VERTEX_POINT('',#6633);
#1918=VERTEX_POINT('',#6657);
#1919=VERTEX_POINT('',#6658);
#1920=VERTEX_POINT('',#6682);
#1921=VERTEX_POINT('',#6683);
#1922=VERTEX_POINT('',#6706);
#1923=VERTEX_POINT('',#6707);
#1924=VERTEX_POINT('',#6709);
#1925=VERTEX_POINT('',#6715);
#1926=VERTEX_POINT('',#7652);
#1927=VERTEX_POINT('',#7655);
#1928=VERTEX_POINT('',#7657);
#1929=VERTEX_POINT('',#7660);
#1930=VERTEX_POINT('',#7662);
#1931=VERTEX_POINT('',#7667);
#1932=VERTEX_POINT('',#7671);
#1933=VERTEX_POINT('',#7673);
#2335=EDGE_CURVE('',#1882,#1883,#1180,.T.);
#2336=EDGE_CURVE('',#1883,#1884,#216,.T.);
#2337=EDGE_CURVE('',#1884,#1885,#1641,.F.);
#2338=EDGE_CURVE('',#1885,#1882,#217,.T.);
#2339=EDGE_CURVE('',#1886,#1887,#1181,.T.);
#2340=EDGE_CURVE('',#1887,#1883,#218,.T.);
#2341=EDGE_CURVE('',#1882,#1886,#219,.T.);
#2342=EDGE_CURVE('',#1888,#1889,#1182,.T.);
#2343=EDGE_CURVE('',#1889,#1887,#220,.T.);
#2344=EDGE_CURVE('',#1886,#1888,#221,.T.);
#2345=EDGE_CURVE('',#1890,#1891,#1183,.T.);
#2346=EDGE_CURVE('',#1891,#1889,#222,.T.);
#2347=EDGE_CURVE('',#1888,#1890,#223,.T.);
#2348=EDGE_CURVE('',#1892,#1893,#1184,.T.);
#2349=EDGE_CURVE('',#1893,#1891,#224,.T.);
#2350=EDGE_CURVE('',#1890,#1892,#225,.T.);
#2351=EDGE_CURVE('',#1894,#1895,#1185,.T.);
#2352=EDGE_CURVE('',#1895,#1893,#226,.T.);
#2353=EDGE_CURVE('',#1892,#1894,#227,.T.);
#2354=EDGE_CURVE('',#1896,#1897,#1186,.T.);
#2355=EDGE_CURVE('',#1897,#1895,#228,.T.);
#2356=EDGE_CURVE('',#1894,#1896,#229,.T.);
#2357=EDGE_CURVE('',#1898,#1899,#1187,.T.);
#2358=EDGE_CURVE('',#1899,#1897,#230,.T.);
#2359=EDGE_CURVE('',#1896,#1898,#231,.T.);
#2360=EDGE_CURVE('',#1900,#1901,#1188,.T.);
#2361=EDGE_CURVE('',#1900,#1902,#232,.T.);
#2362=EDGE_CURVE('',#1903,#1902,#1642,.F.);
#2363=EDGE_CURVE('',#1903,#1901,#233,.T.);
#2364=EDGE_CURVE('',#1904,#1905,#1189,.T.);
#2365=EDGE_CURVE('',#1905,#1906,#234,.T.);
#2366=EDGE_CURVE('',#1907,#1906,#1643,.T.);
#2367=EDGE_CURVE('',#1904,#1907,#235,.T.);
#2368=EDGE_CURVE('',#1908,#1909,#1190,.T.);
#2369=EDGE_CURVE('',#1909,#1905,#236,.T.);
#2370=EDGE_CURVE('',#1908,#1904,#237,.T.);
#2371=EDGE_CURVE('',#1910,#1911,#1191,.T.);
#2372=EDGE_CURVE('',#1911,#1909,#238,.T.);
#2373=EDGE_CURVE('',#1910,#1908,#239,.T.);
#2374=EDGE_CURVE('',#1912,#1913,#1192,.T.);
#2375=EDGE_CURVE('',#1913,#1911,#240,.T.);
#2376=EDGE_CURVE('',#1912,#1910,#241,.T.);
#2377=EDGE_CURVE('',#1914,#1915,#1193,.T.);
#2378=EDGE_CURVE('',#1915,#1913,#242,.T.);
#2379=EDGE_CURVE('',#1914,#1912,#243,.T.);
#2380=EDGE_CURVE('',#1916,#1917,#1194,.T.);
#2381=EDGE_CURVE('',#1917,#1915,#244,.T.);
#2382=EDGE_CURVE('',#1916,#1914,#245,.T.);
#2383=EDGE_CURVE('',#1918,#1919,#1195,.T.);
#2384=EDGE_CURVE('',#1919,#1917,#246,.T.);
#2385=EDGE_CURVE('',#1918,#1916,#247,.T.);
#2386=EDGE_CURVE('',#1920,#1921,#1196,.T.);
#2387=EDGE_CURVE('',#1921,#1919,#248,.T.);
#2388=EDGE_CURVE('',#1920,#1918,#249,.T.);
#2389=EDGE_CURVE('',#1922,#1923,#1197,.T.);
#2390=EDGE_CURVE('',#1924,#1922,#250,.T.);
#2391=EDGE_CURVE('',#1925,#1924,#1644,.T.);
#2392=EDGE_CURVE('',#1925,#1923,#251,.T.);
#2393=EDGE_CURVE('',#1923,#1921,#252,.T.);
#2394=EDGE_CURVE('',#1922,#1920,#253,.T.);
#2395=EDGE_CURVE('',#1906,#1903,#254,.T.);
#2396=EDGE_CURVE('',#1884,#1925,#255,.T.);
#2397=EDGE_CURVE('',#1901,#1899,#256,.T.);
#2398=EDGE_CURVE('',#1902,#1907,#257,.T.);
#2399=EDGE_CURVE('',#1898,#1900,#258,.T.);
#2400=EDGE_CURVE('',#1924,#1885,#259,.T.);
#2401=EDGE_CURVE('',#1926,#1926,#1645,.T.);
#2402=EDGE_CURVE('',#1927,#1927,#1646,.T.);
#2403=EDGE_CURVE('',#1928,#1928,#1647,.T.);
#2404=EDGE_CURVE('',#1929,#1929,#1648,.T.);
#2405=EDGE_CURVE('',#1930,#1930,#1649,.T.);
#2406=EDGE_CURVE('',#1927,#1929,#1198,.T.);
#2407=EDGE_CURVE('',#1930,#1931,#1199,.T.);
#2408=EDGE_CURVE('',#1931,#1931,#1650,.T.);
#2409=EDGE_CURVE('',#1932,#1932,#1651,.T.);
#2410=EDGE_CURVE('',#1933,#1933,#1652,.T.);
#2411=EDGE_CURVE('',#1926,#1932,#1200,.T.);
#2412=EDGE_CURVE('',#1933,#1928,#1201,.T.);
#3181=ORIENTED_EDGE('',*,*,#2335,.T.);
#3182=ORIENTED_EDGE('',*,*,#2336,.T.);
#3183=ORIENTED_EDGE('',*,*,#2337,.T.);
#3184=ORIENTED_EDGE('',*,*,#2338,.T.);
#3185=ORIENTED_EDGE('',*,*,#2339,.T.);
#3186=ORIENTED_EDGE('',*,*,#2340,.T.);
#3187=ORIENTED_EDGE('',*,*,#2335,.F.);
#3188=ORIENTED_EDGE('',*,*,#2341,.T.);
#3189=ORIENTED_EDGE('',*,*,#2342,.T.);
#3190=ORIENTED_EDGE('',*,*,#2343,.T.);
#3191=ORIENTED_EDGE('',*,*,#2339,.F.);
#3192=ORIENTED_EDGE('',*,*,#2344,.T.);
#3193=ORIENTED_EDGE('',*,*,#2345,.T.);
#3194=ORIENTED_EDGE('',*,*,#2346,.T.);
#3195=ORIENTED_EDGE('',*,*,#2342,.F.);
#3196=ORIENTED_EDGE('',*,*,#2347,.T.);
#3197=ORIENTED_EDGE('',*,*,#2348,.T.);
#3198=ORIENTED_EDGE('',*,*,#2349,.T.);
#3199=ORIENTED_EDGE('',*,*,#2345,.F.);
#3200=ORIENTED_EDGE('',*,*,#2350,.T.);
#3201=ORIENTED_EDGE('',*,*,#2351,.T.);
#3202=ORIENTED_EDGE('',*,*,#2352,.T.);
#3203=ORIENTED_EDGE('',*,*,#2348,.F.);
#3204=ORIENTED_EDGE('',*,*,#2353,.T.);
#3205=ORIENTED_EDGE('',*,*,#2354,.T.);
#3206=ORIENTED_EDGE('',*,*,#2355,.T.);
#3207=ORIENTED_EDGE('',*,*,#2351,.F.);
#3208=ORIENTED_EDGE('',*,*,#2356,.T.);
#3209=ORIENTED_EDGE('',*,*,#2357,.T.);
#3210=ORIENTED_EDGE('',*,*,#2358,.T.);
#3211=ORIENTED_EDGE('',*,*,#2354,.F.);
#3212=ORIENTED_EDGE('',*,*,#2359,.T.);
#3213=ORIENTED_EDGE('',*,*,#2360,.F.);
#3214=ORIENTED_EDGE('',*,*,#2361,.T.);
#3215=ORIENTED_EDGE('',*,*,#2362,.F.);
#3216=ORIENTED_EDGE('',*,*,#2363,.T.);
#3217=ORIENTED_EDGE('',*,*,#2364,.T.);
#3218=ORIENTED_EDGE('',*,*,#2365,.T.);
#3219=ORIENTED_EDGE('',*,*,#2366,.F.);
#3220=ORIENTED_EDGE('',*,*,#2367,.F.);
#3221=ORIENTED_EDGE('',*,*,#2368,.T.);
#3222=ORIENTED_EDGE('',*,*,#2369,.T.);
#3223=ORIENTED_EDGE('',*,*,#2364,.F.);
#3224=ORIENTED_EDGE('',*,*,#2370,.F.);
#3225=ORIENTED_EDGE('',*,*,#2371,.T.);
#3226=ORIENTED_EDGE('',*,*,#2372,.T.);
#3227=ORIENTED_EDGE('',*,*,#2368,.F.);
#3228=ORIENTED_EDGE('',*,*,#2373,.F.);
#3229=ORIENTED_EDGE('',*,*,#2374,.T.);
#3230=ORIENTED_EDGE('',*,*,#2375,.T.);
#3231=ORIENTED_EDGE('',*,*,#2371,.F.);
#3232=ORIENTED_EDGE('',*,*,#2376,.F.);
#3233=ORIENTED_EDGE('',*,*,#2377,.T.);
#3234=ORIENTED_EDGE('',*,*,#2378,.T.);
#3235=ORIENTED_EDGE('',*,*,#2374,.F.);
#3236=ORIENTED_EDGE('',*,*,#2379,.F.);
#3237=ORIENTED_EDGE('',*,*,#2380,.T.);
#3238=ORIENTED_EDGE('',*,*,#2381,.T.);
#3239=ORIENTED_EDGE('',*,*,#2377,.F.);
#3240=ORIENTED_EDGE('',*,*,#2382,.F.);
#3241=ORIENTED_EDGE('',*,*,#2383,.T.);
#3242=ORIENTED_EDGE('',*,*,#2384,.T.);
#3243=ORIENTED_EDGE('',*,*,#2380,.F.);
#3244=ORIENTED_EDGE('',*,*,#2385,.F.);
#3245=ORIENTED_EDGE('',*,*,#2386,.T.);
#3246=ORIENTED_EDGE('',*,*,#2387,.T.);
#3247=ORIENTED_EDGE('',*,*,#2383,.F.);
#3248=ORIENTED_EDGE('',*,*,#2388,.F.);
#3249=ORIENTED_EDGE('',*,*,#2389,.F.);
#3250=ORIENTED_EDGE('',*,*,#2390,.F.);
#3251=ORIENTED_EDGE('',*,*,#2391,.F.);
#3252=ORIENTED_EDGE('',*,*,#2392,.T.);
#3253=ORIENTED_EDGE('',*,*,#2389,.T.);
#3254=ORIENTED_EDGE('',*,*,#2393,.T.);
#3255=ORIENTED_EDGE('',*,*,#2386,.F.);
#3256=ORIENTED_EDGE('',*,*,#2394,.F.);
#3257=ORIENTED_EDGE('',*,*,#2395,.F.);
#3258=ORIENTED_EDGE('',*,*,#2365,.F.);
#3259=ORIENTED_EDGE('',*,*,#2369,.F.);
#3260=ORIENTED_EDGE('',*,*,#2372,.F.);
#3261=ORIENTED_EDGE('',*,*,#2375,.F.);
#3262=ORIENTED_EDGE('',*,*,#2378,.F.);
#3263=ORIENTED_EDGE('',*,*,#2381,.F.);
#3264=ORIENTED_EDGE('',*,*,#2384,.F.);
#3265=ORIENTED_EDGE('',*,*,#2387,.F.);
#3266=ORIENTED_EDGE('',*,*,#2393,.F.);
#3267=ORIENTED_EDGE('',*,*,#2392,.F.);
#3268=ORIENTED_EDGE('',*,*,#2396,.F.);
#3269=ORIENTED_EDGE('',*,*,#2336,.F.);
#3270=ORIENTED_EDGE('',*,*,#2340,.F.);
#3271=ORIENTED_EDGE('',*,*,#2343,.F.);
#3272=ORIENTED_EDGE('',*,*,#2346,.F.);
#3273=ORIENTED_EDGE('',*,*,#2349,.F.);
#3274=ORIENTED_EDGE('',*,*,#2352,.F.);
#3275=ORIENTED_EDGE('',*,*,#2355,.F.);
#3276=ORIENTED_EDGE('',*,*,#2358,.F.);
#3277=ORIENTED_EDGE('',*,*,#2397,.F.);
#3278=ORIENTED_EDGE('',*,*,#2363,.F.);
#3279=ORIENTED_EDGE('',*,*,#2398,.F.);
#3280=ORIENTED_EDGE('',*,*,#2361,.F.);
#3281=ORIENTED_EDGE('',*,*,#2399,.F.);
#3282=ORIENTED_EDGE('',*,*,#2359,.F.);
#3283=ORIENTED_EDGE('',*,*,#2356,.F.);
#3284=ORIENTED_EDGE('',*,*,#2353,.F.);
#3285=ORIENTED_EDGE('',*,*,#2350,.F.);
#3286=ORIENTED_EDGE('',*,*,#2347,.F.);
#3287=ORIENTED_EDGE('',*,*,#2344,.F.);
#3288=ORIENTED_EDGE('',*,*,#2341,.F.);
#3289=ORIENTED_EDGE('',*,*,#2338,.F.);
#3290=ORIENTED_EDGE('',*,*,#2400,.F.);
#3291=ORIENTED_EDGE('',*,*,#2390,.T.);
#3292=ORIENTED_EDGE('',*,*,#2394,.T.);
#3293=ORIENTED_EDGE('',*,*,#2388,.T.);
#3294=ORIENTED_EDGE('',*,*,#2385,.T.);
#3295=ORIENTED_EDGE('',*,*,#2382,.T.);
#3296=ORIENTED_EDGE('',*,*,#2379,.T.);
#3297=ORIENTED_EDGE('',*,*,#2376,.T.);
#3298=ORIENTED_EDGE('',*,*,#2373,.T.);
#3299=ORIENTED_EDGE('',*,*,#2370,.T.);
#3300=ORIENTED_EDGE('',*,*,#2367,.T.);
#3301=ORIENTED_EDGE('',*,*,#2401,.T.);
#3302=ORIENTED_EDGE('',*,*,#2398,.T.);
#3303=ORIENTED_EDGE('',*,*,#2366,.T.);
#3304=ORIENTED_EDGE('',*,*,#2395,.T.);
#3305=ORIENTED_EDGE('',*,*,#2362,.T.);
#3306=ORIENTED_EDGE('',*,*,#2402,.T.);
#3307=ORIENTED_EDGE('',*,*,#2403,.F.);
#3308=ORIENTED_EDGE('',*,*,#2404,.F.);
#3309=ORIENTED_EDGE('',*,*,#2405,.F.);
#3310=ORIENTED_EDGE('',*,*,#2402,.F.);
#3311=ORIENTED_EDGE('',*,*,#2406,.T.);
#3312=ORIENTED_EDGE('',*,*,#2404,.T.);
#3313=ORIENTED_EDGE('',*,*,#2406,.F.);
#3314=ORIENTED_EDGE('',*,*,#2405,.T.);
#3315=ORIENTED_EDGE('',*,*,#2407,.T.);
#3316=ORIENTED_EDGE('',*,*,#2408,.T.);
#3317=ORIENTED_EDGE('',*,*,#2407,.F.);
#3318=ORIENTED_EDGE('',*,*,#2409,.F.);
#3319=ORIENTED_EDGE('',*,*,#2410,.T.);
#3320=ORIENTED_EDGE('',*,*,#2401,.F.);
#3321=ORIENTED_EDGE('',*,*,#2411,.T.);
#3322=ORIENTED_EDGE('',*,*,#2409,.T.);
#3323=ORIENTED_EDGE('',*,*,#2411,.F.);
#3324=ORIENTED_EDGE('',*,*,#2360,.T.);
#3325=ORIENTED_EDGE('',*,*,#2397,.T.);
#3326=ORIENTED_EDGE('',*,*,#2357,.F.);
#3327=ORIENTED_EDGE('',*,*,#2399,.T.);
#3328=ORIENTED_EDGE('',*,*,#2410,.F.);
#3329=ORIENTED_EDGE('',*,*,#2412,.T.);
#3330=ORIENTED_EDGE('',*,*,#2403,.T.);
#3331=ORIENTED_EDGE('',*,*,#2412,.F.);
#3332=ORIENTED_EDGE('',*,*,#2408,.F.);
#3333=ORIENTED_EDGE('',*,*,#2400,.T.);
#3334=ORIENTED_EDGE('',*,*,#2337,.F.);
#3335=ORIENTED_EDGE('',*,*,#2396,.T.);
#3336=ORIENTED_EDGE('',*,*,#2391,.T.);
#3593=CYLINDRICAL_SURFACE('',#4217,2.5175);
#3594=CYLINDRICAL_SURFACE('',#4219,2.5175);
#3595=CYLINDRICAL_SURFACE('',#4220,2.5175);
#3596=CYLINDRICAL_SURFACE('',#4221,2.5175);
#3597=CYLINDRICAL_SURFACE('',#4222,2.5175);
#3598=CYLINDRICAL_SURFACE('',#4223,2.5175);
#3599=CYLINDRICAL_SURFACE('',#4224,2.5175);
#3600=CYLINDRICAL_SURFACE('',#4225,2.5175);
#3601=CYLINDRICAL_SURFACE('',#4226,2.5175);
#3602=CYLINDRICAL_SURFACE('',#4228,3.0735);
#3603=CYLINDRICAL_SURFACE('',#4230,3.0735);
#3604=CYLINDRICAL_SURFACE('',#4231,3.0735);
#3605=CYLINDRICAL_SURFACE('',#4232,3.0735);
#3606=CYLINDRICAL_SURFACE('',#4233,3.0735);
#3607=CYLINDRICAL_SURFACE('',#4234,3.0735);
#3608=CYLINDRICAL_SURFACE('',#4235,3.0735);
#3609=CYLINDRICAL_SURFACE('',#4236,3.0735);
#3610=CYLINDRICAL_SURFACE('',#4237,3.0735);
#3611=CYLINDRICAL_SURFACE('',#4239,3.0735);
#3612=CYLINDRICAL_SURFACE('',#4248,7.);
#3613=CYLINDRICAL_SURFACE('',#4249,5.);
#3614=CYLINDRICAL_SURFACE('',#4254,7.);
#3615=CYLINDRICAL_SURFACE('',#4255,2.5175);
#3616=CYLINDRICAL_SURFACE('',#4256,5.);
#3771=ADVANCED_FACE('',(#631),#3593,.F.);
#3772=ADVANCED_FACE('',(#632),#3594,.F.);
#3773=ADVANCED_FACE('',(#633),#3595,.F.);
#3774=ADVANCED_FACE('',(#634),#3596,.F.);
#3775=ADVANCED_FACE('',(#635),#3597,.F.);
#3776=ADVANCED_FACE('',(#636),#3598,.F.);
#3777=ADVANCED_FACE('',(#637),#3599,.F.);
#3778=ADVANCED_FACE('',(#638),#3600,.F.);
#3779=ADVANCED_FACE('',(#639),#3601,.F.);
#3780=ADVANCED_FACE('',(#640),#3602,.F.);
#3781=ADVANCED_FACE('',(#641),#3603,.F.);
#3782=ADVANCED_FACE('',(#642),#3604,.F.);
#3783=ADVANCED_FACE('',(#643),#3605,.F.);
#3784=ADVANCED_FACE('',(#644),#3606,.F.);
#3785=ADVANCED_FACE('',(#645),#3607,.F.);
#3786=ADVANCED_FACE('',(#646),#3608,.F.);
#3787=ADVANCED_FACE('',(#647),#3609,.F.);
#3788=ADVANCED_FACE('',(#648),#3610,.F.);
#3789=ADVANCED_FACE('',(#649),#3611,.F.);
#3790=ADVANCED_FACE('',(#650),#212,.F.);
#3791=ADVANCED_FACE('',(#651),#213,.F.);
#3792=ADVANCED_FACE('',(#652,#403),#487,.T.);
#3793=ADVANCED_FACE('',(#653,#404),#488,.T.);
#3794=ADVANCED_FACE('',(#654,#405),#489,.F.);
#3795=ADVANCED_FACE('',(#655),#3612,.T.);
#3796=ADVANCED_FACE('',(#656),#3613,.T.);
#3797=ADVANCED_FACE('',(#657,#406),#490,.F.);
#3798=ADVANCED_FACE('',(#658),#3614,.T.);
#3799=ADVANCED_FACE('',(#659),#3615,.F.);
#3800=ADVANCED_FACE('',(#660),#3616,.T.);
#3801=ADVANCED_FACE('',(#661,#407),#491,.F.);
#3849=CLOSED_SHELL('',(#3771,#3772,#3773,#3774,#3775,#3776,#3777,#3778,
#3779,#3780,#3781,#3782,#3783,#3784,#3785,#3786,#3787,#3788,#3789,#3790,
#3791,#3792,#3793,#3794,#3795,#3796,#3797,#3798,#3799,#3800,#3801));
#4216=AXIS2_PLACEMENT_3D('',#6097,#5067,#5068);
#4217=AXIS2_PLACEMENT_3D('',#6098,#5069,#5070);
#4218=AXIS2_PLACEMENT_3D('',#6117,#5072,#5073);
#4219=AXIS2_PLACEMENT_3D('',#6137,#5074,#5075);
#4220=AXIS2_PLACEMENT_3D('',#6188,#5077,#5078);
#4221=AXIS2_PLACEMENT_3D('',#6239,#5080,#5081);
#4222=AXIS2_PLACEMENT_3D('',#6287,#5083,#5084);
#4223=AXIS2_PLACEMENT_3D('',#6338,#5086,#5087);
#4224=AXIS2_PLACEMENT_3D('',#6389,#5089,#5090);
#4225=AXIS2_PLACEMENT_3D('',#6437,#5092,#5093);
#4226=AXIS2_PLACEMENT_3D('',#6488,#5095,#5096);
#4227=AXIS2_PLACEMENT_3D('',#6498,#5098,#5099);
#4228=AXIS2_PLACEMENT_3D('',#6509,#5100,#5101);
#4229=AXIS2_PLACEMENT_3D('',#6523,#5103,#5104);
#4230=AXIS2_PLACEMENT_3D('',#6533,#5105,#5106);
#4231=AXIS2_PLACEMENT_3D('',#6557,#5108,#5109);
#4232=AXIS2_PLACEMENT_3D('',#6582,#5111,#5112);
#4233=AXIS2_PLACEMENT_3D('',#6607,#5114,#5115);
#4234=AXIS2_PLACEMENT_3D('',#6631,#5117,#5118);
#4235=AXIS2_PLACEMENT_3D('',#6656,#5120,#5121);
#4236=AXIS2_PLACEMENT_3D('',#6681,#5123,#5124);
#4237=AXIS2_PLACEMENT_3D('',#6705,#5126,#5127);
#4238=AXIS2_PLACEMENT_3D('',#6716,#5129,#5130);
#4239=AXIS2_PLACEMENT_3D('',#6722,#5131,#5132);
#4240=AXIS2_PLACEMENT_3D('',#7651,#5133,#5134);
#4241=AXIS2_PLACEMENT_3D('',#7653,#5135,#5136);
#4242=AXIS2_PLACEMENT_3D('',#7654,#5137,#5138);
#4243=AXIS2_PLACEMENT_3D('',#7656,#5139,#5140);
#4244=AXIS2_PLACEMENT_3D('',#7658,#5141,#5142);
#4245=AXIS2_PLACEMENT_3D('',#7659,#5143,#5144);
#4246=AXIS2_PLACEMENT_3D('',#7661,#5145,#5146);
#4247=AXIS2_PLACEMENT_3D('',#7663,#5147,#5148);
#4248=AXIS2_PLACEMENT_3D('',#7664,#5149,#5150);
#4249=AXIS2_PLACEMENT_3D('',#7666,#5152,#5153);
#4250=AXIS2_PLACEMENT_3D('',#7669,#5155,#5156);
#4251=AXIS2_PLACEMENT_3D('',#7670,#5157,#5158);
#4252=AXIS2_PLACEMENT_3D('',#7672,#5159,#5160);
#4253=AXIS2_PLACEMENT_3D('',#7674,#5161,#5162);
#4254=AXIS2_PLACEMENT_3D('',#7675,#5163,#5164);
#4255=AXIS2_PLACEMENT_3D('',#7677,#5166,#5167);
#4256=AXIS2_PLACEMENT_3D('',#7678,#5168,#5169);
#4257=AXIS2_PLACEMENT_3D('',#7680,#5171,#5172);
#5067=DIRECTION('axis',(0.,0.,1.));
#5068=DIRECTION('refdir',(1.,0.,0.));
#5069=DIRECTION('center_axis',(0.,0.,1.));
#5070=DIRECTION('ref_axis',(0.938002329630376,0.346628950908588,0.));
#5071=DIRECTION('',(0.,0.,-1.));
#5072=DIRECTION('center_axis',(0.,0.,1.));
#5073=DIRECTION('ref_axis',(1.,0.,0.));
#5074=DIRECTION('center_axis',(0.,0.,1.));
#5075=DIRECTION('ref_axis',(1.,0.,0.));
#5076=DIRECTION('',(0.,0.,-1.));
#5077=DIRECTION('center_axis',(0.,0.,1.));
#5078=DIRECTION('ref_axis',(1.,0.,0.));
#5079=DIRECTION('',(0.,0.,-1.));
#5080=DIRECTION('center_axis',(0.,0.,1.));
#5081=DIRECTION('ref_axis',(1.,0.,0.));
#5082=DIRECTION('',(0.,0.,-1.));
#5083=DIRECTION('center_axis',(0.,0.,1.));
#5084=DIRECTION('ref_axis',(1.,0.,0.));
#5085=DIRECTION('',(0.,0.,-1.));
#5086=DIRECTION('center_axis',(0.,0.,1.));
#5087=DIRECTION('ref_axis',(1.,0.,0.));
#5088=DIRECTION('',(0.,0.,-1.));
#5089=DIRECTION('center_axis',(0.,0.,1.));
#5090=DIRECTION('ref_axis',(1.,0.,0.));
#5091=DIRECTION('',(0.,0.,-1.));
#5092=DIRECTION('center_axis',(0.,0.,1.));
#5093=DIRECTION('ref_axis',(1.,0.,0.));
#5094=DIRECTION('',(0.,0.,-1.));
#5095=DIRECTION('center_axis',(0.,0.,1.));
#5096=DIRECTION('ref_axis',(-0.346901083835764,-0.937901720882083,0.));
#5097=DIRECTION('',(0.,0.,-1.));
#5098=DIRECTION('center_axis',(0.,0.,1.));
#5099=DIRECTION('ref_axis',(1.,0.,0.));
#5100=DIRECTION('center_axis',(0.,0.,1.));
#5101=DIRECTION('ref_axis',(1.,4.65526718641507E-14,0.));
#5102=DIRECTION('',(1.22464679914735E-16,5.71605565684554E-30,1.));
#5103=DIRECTION('center_axis',(0.,0.,-1.));
#5104=DIRECTION('ref_axis',(1.,4.65526718641507E-14,0.));
#5105=DIRECTION('center_axis',(0.,0.,1.));
#5106=DIRECTION('ref_axis',(1.,4.65526718641507E-14,0.));
#5107=DIRECTION('',(1.22464679914735E-16,5.71605565684554E-30,1.));
#5108=DIRECTION('center_axis',(0.,0.,1.));
#5109=DIRECTION('ref_axis',(1.,4.65526718641507E-14,0.));
#5110=DIRECTION('',(1.22464679914735E-16,5.71605565684554E-30,1.));
#5111=DIRECTION('center_axis',(0.,0.,1.));
#5112=DIRECTION('ref_axis',(1.,4.65526718641507E-14,0.));
#5113=DIRECTION('',(1.22464679914735E-16,5.71605565684554E-30,1.));
#5114=DIRECTION('center_axis',(0.,0.,1.));
#5115=DIRECTION('ref_axis',(1.,4.65526718641507E-14,0.));
#5116=DIRECTION('',(1.22464679914735E-16,5.71605565684554E-30,1.));
#5117=DIRECTION('center_axis',(0.,0.,1.));
#5118=DIRECTION('ref_axis',(1.,4.65526718641507E-14,0.));
#5119=DIRECTION('',(1.22464679914735E-16,5.71605565684554E-30,1.));
#5120=DIRECTION('center_axis',(0.,0.,1.));
#5121=DIRECTION('ref_axis',(1.,4.65526718641507E-14,0.));
#5122=DIRECTION('',(1.22464679914735E-16,5.71605565684554E-30,1.));
#5123=DIRECTION('center_axis',(0.,0.,1.));
#5124=DIRECTION('ref_axis',(1.,4.65526718641507E-14,0.));
#5125=DIRECTION('',(1.22464679914735E-16,5.71605565684554E-30,1.));
#5126=DIRECTION('center_axis',(0.,0.,1.));
#5127=DIRECTION('ref_axis',(-0.609180499130755,0.793031600554987,0.));
#5128=DIRECTION('',(1.22464679914735E-16,5.71605565684554E-30,1.));
#5129=DIRECTION('center_axis',(0.,0.,1.));
#5130=DIRECTION('ref_axis',(1.,4.65526718641507E-14,0.));
#5131=DIRECTION('center_axis',(0.,0.,1.));
#5132=DIRECTION('ref_axis',(1.,4.65526718641507E-14,0.));
#5133=DIRECTION('center_axis',(0.,0.,1.));
#5134=DIRECTION('ref_axis',(1.,0.,0.));
#5135=DIRECTION('center_axis',(0.,0.,1.));
#5136=DIRECTION('ref_axis',(1.,0.,0.));
#5137=DIRECTION('center_axis',(0.,0.,1.));
#5138=DIRECTION('ref_axis',(1.,0.,0.));
#5139=DIRECTION('center_axis',(0.,0.,1.));
#5140=DIRECTION('ref_axis',(1.,0.,0.));
#5141=DIRECTION('center_axis',(0.,0.,1.));
#5142=DIRECTION('ref_axis',(1.,0.,0.));
#5143=DIRECTION('center_axis',(0.,0.,1.));
#5144=DIRECTION('ref_axis',(1.,0.,0.));
#5145=DIRECTION('center_axis',(0.,0.,1.));
#5146=DIRECTION('ref_axis',(1.,0.,0.));
#5147=DIRECTION('center_axis',(0.,0.,-1.));
#5148=DIRECTION('ref_axis',(1.,0.,0.));
#5149=DIRECTION('center_axis',(0.,0.,1.));
#5150=DIRECTION('ref_axis',(1.,0.,0.));
#5151=DIRECTION('',(0.,0.,-1.));
#5152=DIRECTION('center_axis',(0.,0.,1.));
#5153=DIRECTION('ref_axis',(1.,0.,0.));
#5154=DIRECTION('',(0.,0.,-1.));
#5155=DIRECTION('center_axis',(0.,0.,1.));
#5156=DIRECTION('ref_axis',(1.,0.,0.));
#5157=DIRECTION('center_axis',(0.,0.,1.));
#5158=DIRECTION('ref_axis',(1.,0.,0.));
#5159=DIRECTION('center_axis',(0.,0.,1.));
#5160=DIRECTION('ref_axis',(1.,0.,0.));
#5161=DIRECTION('center_axis',(0.,0.,1.));
#5162=DIRECTION('ref_axis',(1.,0.,0.));
#5163=DIRECTION('center_axis',(0.,0.,1.));
#5164=DIRECTION('ref_axis',(1.,0.,0.));
#5165=DIRECTION('',(0.,0.,-1.));
#5166=DIRECTION('center_axis',(0.,0.,1.));
#5167=DIRECTION('ref_axis',(1.,0.,0.));
#5168=DIRECTION('center_axis',(0.,0.,1.));
#5169=DIRECTION('ref_axis',(1.,0.,0.));
#5170=DIRECTION('',(0.,0.,-1.));
#5171=DIRECTION('center_axis',(0.,0.,1.));
#5172=DIRECTION('ref_axis',(1.,0.,0.));
#6097=CARTESIAN_POINT('',(0.,0.,0.));
#6098=CARTESIAN_POINT('Origin',(0.,0.,0.));
#6099=CARTESIAN_POINT('',(-2.51487600649923,-0.00174710143214298,0.887416697508018));
#6100=CARTESIAN_POINT('',(-2.52011424653381,-0.00155468419460097,0.612583302491977));
#6101=CARTESIAN_POINT('',(-2.5175,-3.08304831685346E-16,0.));
#6102=CARTESIAN_POINT('',(1.91346599666506,-1.63598720337495,0.));
#6103=CARTESIAN_POINT('Ctrl Pts',(-2.52011424653381,-0.00155468419460097,
0.612583302491977));
#6104=CARTESIAN_POINT('Ctrl Pts',(-2.51459953682427,0.727061179433973,0.566372033576619));
#6105=CARTESIAN_POINT('Ctrl Pts',(-2.18058200222388,1.45987955194242,0.520160764661261));
#6106=CARTESIAN_POINT('Ctrl Pts',(-1.62389475685714,1.92874616523596,0.473949495745903));
#6107=CARTESIAN_POINT('Ctrl Pts',(-0.98950971657857,2.46305329699636,0.421288440663024));
#6108=CARTESIAN_POINT('Ctrl Pts',(-0.0659605128080866,2.65458641879863,
0.368627385580146));
#6109=CARTESIAN_POINT('Ctrl Pts',(0.728030814102273,2.41463261372602,0.315966330497268));
#6110=CARTESIAN_POINT('Ctrl Pts',(1.52202214101263,2.17467880865341,0.26330527541439));
#6111=CARTESIAN_POINT('Ctrl Pts',(2.18645559106287,1.50323807670592,0.210644220331512));
#6112=CARTESIAN_POINT('Ctrl Pts',(2.41964507597276,0.708853082730267,0.157983165248634));
#6113=CARTESIAN_POINT('Ctrl Pts',(2.65283456088265,-0.0855319112453835,
0.105322110165756));
#6114=CARTESIAN_POINT('Ctrl Pts',(2.45478008065218,-1.00286116724919,0.0526610550828779));
#6115=CARTESIAN_POINT('Ctrl Pts',(1.91346599666506,-1.63598720337495,-2.77555756156289E-16));
#6116=CARTESIAN_POINT('',(-1.91703660311682,-1.63861995150711,-4.84824442051532E-16));
#6117=CARTESIAN_POINT('Origin',(0.,0.,0.));
#6118=CARTESIAN_POINT('Ctrl Pts',(-1.91704123069775,-1.63862336360397,-2.77555756156289E-16));
#6119=CARTESIAN_POINT('Ctrl Pts',(-1.39386687448522,-2.24786647282135,0.0509809153588233));
#6120=CARTESIAN_POINT('Ctrl Pts',(-0.55338302340234,-2.58772319466498,0.101961830717647));
#6121=CARTESIAN_POINT('Ctrl Pts',(0.245732972111121,-2.5093256741233,0.15294274607647));
#6122=CARTESIAN_POINT('Ctrl Pts',(1.07118483308992,-2.42834446539943,0.205603801159349));
#6123=CARTESIAN_POINT('Ctrl Pts',(1.85249724960843,-1.90108656072576,0.258264856242227));
#6124=CARTESIAN_POINT('Ctrl Pts',(2.23581596847939,-1.16587048520445,0.310925911325105));
#6125=CARTESIAN_POINT('Ctrl Pts',(2.61913468735035,-0.430654409683135,0.363586966407983));
#6126=CARTESIAN_POINT('Ctrl Pts',(2.60445970857376,0.512519836685811,0.416248021490861));
#6127=CARTESIAN_POINT('Ctrl Pts',(2.19819451399913,1.23549094635129,0.468909076573739));
#6128=CARTESIAN_POINT('Ctrl Pts',(1.7919293194245,1.95846205601678,0.521570131656618));
#6129=CARTESIAN_POINT('Ctrl Pts',(0.994073909051824,2.46123002897879,0.574231186739496));
#6130=CARTESIAN_POINT('Ctrl Pts',(0.166600790821099,2.51599781963901,0.626892241822374));
#6131=CARTESIAN_POINT('Ctrl Pts',(-0.660872327409628,2.57076561029922,0.679553296905252));
#6132=CARTESIAN_POINT('Ctrl Pts',(-1.5179631534984,2.17753321865762,0.732214351988131));
#6133=CARTESIAN_POINT('Ctrl Pts',(-2.01603503865931,1.51452501467868,0.784875407071009));
#6134=CARTESIAN_POINT('Ctrl Pts',(-2.33931590060693,1.08418981599261,0.819055837216678));
#6135=CARTESIAN_POINT('Ctrl Pts',(-2.51134748918236,0.540202130103611,0.853236267362348));
#6136=CARTESIAN_POINT('Ctrl Pts',(-2.51487600649923,-0.00174710143214298,
0.887416697508018));
#6137=CARTESIAN_POINT('Origin',(0.,0.,0.));
#6138=CARTESIAN_POINT('',(-2.52149019825988,-0.000319702518148003,1.88741669750802));
#6139=CARTESIAN_POINT('',(-2.51813779298502,0.00219620146278118,1.61258330249198));
#6140=CARTESIAN_POINT('',(-2.5175,-3.08304831685346E-16,0.));
#6141=CARTESIAN_POINT('Ctrl Pts',(-2.51813779298502,0.00219620146278118,
1.61258330249198));
#6142=CARTESIAN_POINT('Ctrl Pts',(-2.51970373897608,0.174721836780657,1.60166608582343));
#6143=CARTESIAN_POINT('Ctrl Pts',(-2.50346821380307,0.346954441346066,1.59074886915489));
#6144=CARTESIAN_POINT('Ctrl Pts',(-2.46833960002055,0.515242964361496,1.57983165248634));
#6145=CARTESIAN_POINT('Ctrl Pts',(-2.29889074491847,1.32701133439546,1.52717059740347));
#6146=CARTESIAN_POINT('Ctrl Pts',(-1.68984135267922,2.04700961835622,1.47450954232059));
#6147=CARTESIAN_POINT('Ctrl Pts',(-0.917406816181398,2.34872522509939,1.42184848723771));
#6148=CARTESIAN_POINT('Ctrl Pts',(-0.144972279683573,2.65044083184256,1.36918743215483));
#6149=CARTESIAN_POINT('Ctrl Pts',(0.790847401072825,2.53387376136814,1.31652637707195));
#6150=CARTESIAN_POINT('Ctrl Pts',(1.46564413375167,2.05185297138638,1.26386532198907));
#6151=CARTESIAN_POINT('Ctrl Pts',(2.14044086643052,1.56983218140461,1.2112042669062));
#6152=CARTESIAN_POINT('Ctrl Pts',(2.5542146510318,0.7223576719155,1.15854321182332));
#6153=CARTESIAN_POINT('Ctrl Pts',(2.51930798934804,-0.106157141646233,1.10588215674044));
#6154=CARTESIAN_POINT('Ctrl Pts',(2.48440132766427,-0.934671955207963,1.05322110165756));
#6155=CARTESIAN_POINT('Ctrl Pts',(2.00081421969545,-1.74422707284231,1.00056004657468));
#6156=CARTESIAN_POINT('Ctrl Pts',(1.28786937648264,-2.16780796801704,0.947898991491806));
#6157=CARTESIAN_POINT('Ctrl Pts',(0.574924533269827,-2.59138886319177,0.895237936408928));
#6158=CARTESIAN_POINT('Ctrl Pts',(-0.367378045186977,-2.62899553590688,
0.84257688132605));
#6159=CARTESIAN_POINT('Ctrl Pts',(-1.11170282225959,-2.26331904582102,0.789915826243172));
#6160=CARTESIAN_POINT('Ctrl Pts',(-1.8560275993322,-1.89764255573516,0.737254771160294));
#6161=CARTESIAN_POINT('Ctrl Pts',(-2.40237457502062,-1.12868290284834,0.684593716077416));
#6162=CARTESIAN_POINT('Ctrl Pts',(-2.5029376244715,-0.305662505545658,0.631932660994538));
#6163=CARTESIAN_POINT('Ctrl Pts',(-2.51525431968946,-0.204861153089739,
0.625482874827017));
#6164=CARTESIAN_POINT('Ctrl Pts',(-2.52088394403914,-0.10324885163404,0.619033088659497));
#6165=CARTESIAN_POINT('Ctrl Pts',(-2.52011424653381,-0.00155468419460097,
0.612583302491977));
#6166=CARTESIAN_POINT('Ctrl Pts',(-2.51487600649923,-0.00174710143214298,
0.887416697508018));
#6167=CARTESIAN_POINT('Ctrl Pts',(-2.51678380007701,-0.29476741862348,0.905897322445226));
#6168=CARTESIAN_POINT('Ctrl Pts',(-2.46943253823011,-0.587191827768646,
0.924377947382434));
#6169=CARTESIAN_POINT('Ctrl Pts',(-2.37009511448484,-0.860734411891926,
0.942858572319643));
#6170=CARTESIAN_POINT('Ctrl Pts',(-2.08703036091644,-1.64020161816731,0.995519627402521));
#6171=CARTESIAN_POINT('Ctrl Pts',(-1.38184790954662,-2.26635201440178,1.0481806824854));
#6172=CARTESIAN_POINT('Ctrl Pts',(-0.574378778493375,-2.45524661303475,
1.10084173756828));
#6173=CARTESIAN_POINT('Ctrl Pts',(0.233090352559867,-2.64414121166772,1.15350279265116));
#6174=CARTESIAN_POINT('Ctrl Pts',(1.14284616329653,-2.39578001269919,1.20616384773403));
#6175=CARTESIAN_POINT('Ctrl Pts',(1.74230865905524,-1.82278291337913,1.25882490281691));
#6176=CARTESIAN_POINT('Ctrl Pts',(2.34177115481396,-1.24978581405907,1.31148595789979));
#6177=CARTESIAN_POINT('Ctrl Pts',(2.63094033559473,-0.352152814387476,1.36414701298267));
#6178=CARTESIAN_POINT('Ctrl Pts',(2.47866792745056,0.46301576636188,1.41680806806555));
#6179=CARTESIAN_POINT('Ctrl Pts',(2.32639551930638,1.27818434711123,1.46946912314843));
#6180=CARTESIAN_POINT('Ctrl Pts',(1.73268152223725,2.01088850893835,1.5221301782313));
#6181=CARTESIAN_POINT('Ctrl Pts',(0.966788038826866,2.32883881680251,1.57479123331418));
#6182=CARTESIAN_POINT('Ctrl Pts',(0.200894555416484,2.64678912466668,1.62745228839706));
#6183=CARTESIAN_POINT('Ctrl Pts',(-0.737178414335148,2.54998557856789,1.68011334347994));
#6184=CARTESIAN_POINT('Ctrl Pts',(-1.42200016567859,2.08232793645304,1.73277439856282));
#6185=CARTESIAN_POINT('Ctrl Pts',(-2.09234000745072,1.6245598395668,1.78432183154455));
#6186=CARTESIAN_POINT('Ctrl Pts',(-2.52002637342648,0.811456688510852,1.83586926452628));
#6187=CARTESIAN_POINT('Ctrl Pts',(-2.52149019825988,-0.000319702518148003,
1.88741669750802));
#6188=CARTESIAN_POINT('Origin',(0.,0.,0.));
#6189=CARTESIAN_POINT('',(-2.51571955069522,0.0020516094281591,2.88741669750802));
#6190=CARTESIAN_POINT('',(-2.51355581944505,-0.000494562389464492,2.61258330249198));
#6191=CARTESIAN_POINT('',(-2.5175,-3.08304831685346E-16,0.));
#6192=CARTESIAN_POINT('Ctrl Pts',(-2.51355581944505,-0.000494562389464492,
2.61258330249198));
#6193=CARTESIAN_POINT('Ctrl Pts',(-2.51275958993137,0.448550632625545,2.58429908298737));
#6194=CARTESIAN_POINT('Ctrl Pts',(-2.39795577577843,0.897975827471433,2.55601486348276));
#6195=CARTESIAN_POINT('Ctrl Pts',(-2.17158417223202,1.28155930423489,2.52773064397815));
#6196=CARTESIAN_POINT('Ctrl Pts',(-1.75011355390313,1.99573529892449,2.47506958889527));
#6197=CARTESIAN_POINT('Ctrl Pts',(-0.941893630300218,2.48167123557527,2.42240853381239));
#6198=CARTESIAN_POINT('Ctrl Pts',(-0.113465952320697,2.51898725941957,2.36974747872952));
#6199=CARTESIAN_POINT('Ctrl Pts',(0.714961725658818,2.55630328326386,2.31708642364664));
#6200=CARTESIAN_POINT('Ctrl Pts',(1.56359715801494,2.14499939430168,2.26442536856376));
#6201=CARTESIAN_POINT('Ctrl Pts',(2.04756973616912,1.47160818786419,2.21176431348088));
#6202=CARTESIAN_POINT('Ctrl Pts',(2.53154231432331,0.798216981426686,2.159103258398));
#6203=CARTESIAN_POINT('Ctrl Pts',(2.65085203827557,-0.137261542486132,2.10644220331512));
#6204=CARTESIAN_POINT('Ctrl Pts',(2.35138983004132,-0.910570496909335,2.05378114823225));
#6205=CARTESIAN_POINT('Ctrl Pts',(2.05192762180707,-1.68387945133254,2.00112009314937));
#6206=CARTESIAN_POINT('Ctrl Pts',(1.33369348138632,-2.29501883626613,1.94845903806649));
#6207=CARTESIAN_POINT('Ctrl Pts',(0.522419005839605,-2.46682921151411,1.89579798298361));
#6208=CARTESIAN_POINT('Ctrl Pts',(-0.288855469707103,-2.63863958676209,
1.84313692790073));
#6209=CARTESIAN_POINT('Ctrl Pts',(-1.19317028037977,-2.37112095232446,1.79047587281786));
#6210=CARTESIAN_POINT('Ctrl Pts',(-1.78040352673365,-1.78559240705206,1.73781481773498));
#6211=CARTESIAN_POINT('Ctrl Pts',(-2.24589685398929,-1.32145037757005,1.69607097932064));
#6212=CARTESIAN_POINT('Ctrl Pts',(-2.51215013162399,-0.65748496652123,1.65432714090631));
#6213=CARTESIAN_POINT('Ctrl Pts',(-2.51813779298502,0.00219620146278118,
1.61258330249198));
#6214=CARTESIAN_POINT('Ctrl Pts',(-2.52149019825988,-0.000319702518148003,
1.88741669750802));
#6215=CARTESIAN_POINT('Ctrl Pts',(-2.5215218224862,-0.0178571835903327,
1.88853031960916));
#6216=CARTESIAN_POINT('Ctrl Pts',(-2.52135451775278,-0.0353940454296833,
1.88964394171031));
#6217=CARTESIAN_POINT('Ctrl Pts',(-2.52098643312153,-0.0529266917933569,
1.89075756381145));
#6218=CARTESIAN_POINT('Ctrl Pts',(-2.50358041628578,-0.882011939794007,
1.94341861889433));
#6219=CARTESIAN_POINT('Ctrl Pts',(-2.03719784967901,-1.7016706976644,1.99607967397721));
#6220=CARTESIAN_POINT('Ctrl Pts',(-1.33335156767863,-2.14017435875082,2.04874072906008));
#6221=CARTESIAN_POINT('Ctrl Pts',(-0.629505285678259,-2.57867801983723,
2.10140178414296));
#6222=CARTESIAN_POINT('Ctrl Pts',(0.311804711715729,-2.63602658413966,2.15406283922584));
#6223=CARTESIAN_POINT('Ctrl Pts',(1.06367847532566,-2.28621117073127,2.20672389430872));
#6224=CARTESIAN_POINT('Ctrl Pts',(1.81555223893559,-1.93639575732288,2.2593849493916));
#6225=CARTESIAN_POINT('Ctrl Pts',(2.37798976876147,-1.17941636620366,2.31204600447447));
#6226=CARTESIAN_POINT('Ctrl Pts',(2.49591594240719,-0.358576241429396,2.36470705955735));
#6227=CARTESIAN_POINT('Ctrl Pts',(2.61384211605291,0.462263883344868,2.41736811464023));
#6228=CARTESIAN_POINT('Ctrl Pts',(2.28725693351847,1.34696474177417,2.47002916972311));
#6229=CARTESIAN_POINT('Ctrl Pts',(1.66427240295436,1.89429948580111,2.52269022480599));
#6230=CARTESIAN_POINT('Ctrl Pts',(1.04128787239026,2.44163422982805,2.57535127988887));
#6231=CARTESIAN_POINT('Ctrl Pts',(0.12190399379649,2.65160285945263,2.62801233497175));
#6232=CARTESIAN_POINT('Ctrl Pts',(-0.676922982005502,2.42898097098493,2.68067339005462));
#6233=CARTESIAN_POINT('Ctrl Pts',(-1.47574995780749,2.20635908251724,2.7333344451375));
#6234=CARTESIAN_POINT('Ctrl Pts',(-2.1540200308177,1.55114667595727,2.78599550022038));
#6235=CARTESIAN_POINT('Ctrl Pts',(-2.40412613268695,0.760493784040427,2.83865655530326));
#6236=CARTESIAN_POINT('Ctrl Pts',(-2.48131922521823,0.516465584049649,2.85490993603818));
#6237=CARTESIAN_POINT('Ctrl Pts',(-2.51772563121066,0.259535390913114,2.8711633167731));
#6238=CARTESIAN_POINT('Ctrl Pts',(-2.51571955069522,0.0020516094281591,
2.88741669750802));
#6239=CARTESIAN_POINT('Origin',(0.,0.,0.));
#6240=CARTESIAN_POINT('',(-2.51469328235907,-0.00165890949178153,3.88741669750802));
#6241=CARTESIAN_POINT('',(-2.51988725850616,-0.00173537346078306,3.61258330249198));
#6242=CARTESIAN_POINT('',(-2.5175,-3.08304831685346E-16,0.));
#6243=CARTESIAN_POINT('Ctrl Pts',(-2.51988725850616,-0.00173537346078306,
3.61258330249198));
#6244=CARTESIAN_POINT('Ctrl Pts',(-2.51420136288543,0.718396137764606,3.5669320801513));
#6245=CARTESIAN_POINT('Ctrl Pts',(-2.18921873634932,1.44301231504753,3.52128085781063));
#6246=CARTESIAN_POINT('Ctrl Pts',(-1.64418245628449,1.91176252643724,3.47562963546996));
#6247=CARTESIAN_POINT('Ctrl Pts',(-1.01545481012268,2.4524902317743,3.42296858038708));
#6248=CARTESIAN_POINT('Ctrl Pts',(-0.0939057222003969,2.65274169493656,
3.3703075253042));
#6249=CARTESIAN_POINT('Ctrl Pts',(0.702526568429994,2.42169946773059,3.31764647022132));
#6250=CARTESIAN_POINT('Ctrl Pts',(1.49895885906039,2.19065724052462,3.26498541513844));
#6251=CARTESIAN_POINT('Ctrl Pts',(2.17027435239889,1.52832132295041,3.21232436005557));
#6252=CARTESIAN_POINT('Ctrl Pts',(2.41202001637171,0.73507234206789,3.15966330497269));
#6253=CARTESIAN_POINT('Ctrl Pts',(2.65376568034452,-0.0581766388146221,
3.10700224988981));
#6254=CARTESIAN_POINT('Ctrl Pts',(2.46594151495165,-0.982338683005439,3.05434119480693));
#6255=CARTESIAN_POINT('Ctrl Pts',(1.93372898294791,-1.61829050288557,3.00168013972405));
#6256=CARTESIAN_POINT('Ctrl Pts',(1.40151645094418,-2.2542423227657,2.94901908464117));
#6257=CARTESIAN_POINT('Ctrl Pts',(0.524915552329573,-2.60198391833514,2.8963580295583));
#6258=CARTESIAN_POINT('Ctrl Pts',(-0.298520242041991,-2.50380859645435,
2.84369697447542));
#6259=CARTESIAN_POINT('Ctrl Pts',(-1.12195603641355,-2.40563327457356,2.79103591939254));
#6260=CARTESIAN_POINT('Ctrl Pts',(-1.89222672654207,-1.86154103524254,2.73837486430966));
#6261=CARTESIAN_POINT('Ctrl Pts',(-2.2600014150789,-1.11828688921283,2.68571380922678));
#6262=CARTESIAN_POINT('Ctrl Pts',(-2.43024455012818,-0.774234076709942,
2.66133697364852));
#6263=CARTESIAN_POINT('Ctrl Pts',(-2.51424205213159,-0.387505449655048,
2.63696013807025));
#6264=CARTESIAN_POINT('Ctrl Pts',(-2.51355581944505,-0.000494562389464492,
2.61258330249198));
#6265=CARTESIAN_POINT('Ctrl Pts',(-2.51571955069522,0.0020516094281591,
2.88741669750802));
#6266=CARTESIAN_POINT('Ctrl Pts',(-2.51122591781276,-0.574713669074463,
2.92382437185598));
#6267=CARTESIAN_POINT('Ctrl Pts',(-2.31399271794437,-1.15425664796212,2.96023204620393));
#6268=CARTESIAN_POINT('Ctrl Pts',(-1.95070481508442,-1.59778720918929,2.99663972055189));
#6269=CARTESIAN_POINT('Ctrl Pts',(-1.42523526488438,-2.23932193322841,3.04930077563477));
#6270=CARTESIAN_POINT('Ctrl Pts',(-0.55235403375603,-2.59629800403293,3.10196183071765));
#6271=CARTESIAN_POINT('Ctrl Pts',(0.272072347378842,-2.50682067463764,3.15462288580053));
#6272=CARTESIAN_POINT('Ctrl Pts',(1.09649872851371,-2.41734334524235,3.20728394088341));
#6273=CARTESIAN_POINT('Ctrl Pts',(1.8724702596551,-1.88141261564727,3.25994499596628));
#6274=CARTESIAN_POINT('Ctrl Pts',(2.24807060652927,-1.14208222144429,3.31260605104916));
#6275=CARTESIAN_POINT('Ctrl Pts',(2.62367095340345,-0.402751827241306,3.36526710613204));
#6276=CARTESIAN_POINT('Ctrl Pts',(2.5989001160104,0.539978231569575,3.41792816121491));
#6277=CARTESIAN_POINT('Ctrl Pts',(2.18499209295389,1.25856378644175,3.47058921629779));
#6278=CARTESIAN_POINT('Ctrl Pts',(1.77108406989738,1.97714934131393,3.52325027138067));
#6279=CARTESIAN_POINT('Ctrl Pts',(0.968038861177412,2.4715903922474,3.57591132646355));
#6280=CARTESIAN_POINT('Ctrl Pts',(0.14005117319827,2.5176494835237,3.62857238154643));
#6281=CARTESIAN_POINT('Ctrl Pts',(-0.687936514780865,2.56370857479999,3.68123343662931));
#6282=CARTESIAN_POINT('Ctrl Pts',(-1.54086668201918,2.16138570641911,3.73389449171218));
#6283=CARTESIAN_POINT('Ctrl Pts',(-2.03192094120479,1.49314116576332,3.78655554679506));
#6284=CARTESIAN_POINT('Ctrl Pts',(-2.3454245829758,1.06651397911266,3.82017593036605));
#6285=CARTESIAN_POINT('Ctrl Pts',(-2.51143030795531,0.531499105364158,3.85379631393703));
#6286=CARTESIAN_POINT('Ctrl Pts',(-2.51469328235907,-0.00165890949178153,
3.88741669750802));
#6287=CARTESIAN_POINT('Origin',(0.,0.,0.));
#6288=CARTESIAN_POINT('',(-2.52142713785251,-0.000477745744092403,4.88741669750802));
#6289=CARTESIAN_POINT('',(-2.5184009829045,0.00215602902869219,4.61258330249198));
#6290=CARTESIAN_POINT('',(-2.5175,-3.08304831685346E-16,0.));
#6291=CARTESIAN_POINT('Ctrl Pts',(-2.5184009829045,0.00215602902869219,
4.61258330249198));
#6292=CARTESIAN_POINT('Ctrl Pts',(-2.51987859619477,0.165787052272115,4.60222613239812));
#6293=CARTESIAN_POINT('Ctrl Pts',(-2.50528024663712,0.329155676438073,4.59186896230426));
#6294=CARTESIAN_POINT('Ctrl Pts',(-2.47364099272538,0.489154516809472,4.5815117922104));
#6295=CARTESIAN_POINT('Ctrl Pts',(-2.31277113368779,1.30266898742634,4.52885073712752));
#6296=CARTESIAN_POINT('Ctrl Pts',(-1.71135702808935,2.02906725622667,4.47618968204464));
#6297=CARTESIAN_POINT('Ctrl Pts',(-0.942150236578554,2.33891531144121,4.42352862696176));
#6298=CARTESIAN_POINT('Ctrl Pts',(-0.172943445067766,2.64876336665576,4.37086757187889));
#6299=CARTESIAN_POINT('Ctrl Pts',(0.764056032355369,2.54206120828453,4.31820651679601));
#6300=CARTESIAN_POINT('Ctrl Pts',(1.44390294176358,2.06720008630591,4.26554546171313));
#6301=CARTESIAN_POINT('Ctrl Pts',(2.1237498511718,1.59233896432729,4.21288440663025));
#6302=CARTESIAN_POINT('Ctrl Pts',(2.54644419256509,0.749318878741279,4.16022335154737));
#6303=CARTESIAN_POINT('Ctrl Pts',(2.52028686841065,-0.0795361749092185,
4.10756229646449));
#6304=CARTESIAN_POINT('Ctrl Pts',(2.4941295442562,-0.908391228559711,4.05490124138161));
#6305=CARTESIAN_POINT('Ctrl Pts',(2.01912055455403,-1.72308125027469,4.00224018629874));
#6306=CARTESIAN_POINT('Ctrl Pts',(1.31068458263584,-2.15413041105905,3.94957913121586));
#6307=CARTESIAN_POINT('Ctrl Pts',(0.602248610717651,-2.58517957184342,3.89691807613298));
#6308=CARTESIAN_POINT('Ctrl Pts',(-0.339614343416557,-2.63258787169717,
3.8442570210501));
#6309=CARTESIAN_POINT('Ctrl Pts',(-1.08775335610003,-2.27485483868615,3.79159596596722));
#6310=CARTESIAN_POINT('Ctrl Pts',(-1.83589236878351,-1.91712180567512,3.73893491088435));
#6311=CARTESIAN_POINT('Ctrl Pts',(-2.39030744001625,-1.15424743979932,3.68627385580147));
#6312=CARTESIAN_POINT('Ctrl Pts',(-2.49956187343194,-0.332208283105492,
3.63361280071859));
#6313=CARTESIAN_POINT('Ctrl Pts',(-2.51410497940244,-0.222784782438857,
3.62660296797639));
#6314=CARTESIAN_POINT('Ctrl Pts',(-2.52076033868337,-0.112312948107318,
3.61959313523418));
#6315=CARTESIAN_POINT('Ctrl Pts',(-2.51988725850616,-0.00173537346078306,
3.61258330249198));
#6316=CARTESIAN_POINT('Ctrl Pts',(-2.51469328235907,-0.00165890949178153,
3.88741669750802));
#6317=CARTESIAN_POINT('Ctrl Pts',(-2.51654124532602,-0.303609260634305,
3.90645736901991));
#6318=CARTESIAN_POINT('Ctrl Pts',(-2.46619036907829,-0.604964034533392,
3.92549804053181));
#6319=CARTESIAN_POINT('Ctrl Pts',(-2.36087140795563,-0.885697153183018,
3.9445387120437));
#6320=CARTESIAN_POINT('Ctrl Pts',(-2.06958926438796,-1.66212471854286,3.99719976712658));
#6321=CARTESIAN_POINT('Ctrl Pts',(-1.35784662611974,-2.28081363633185,4.04986082220945));
#6322=CARTESIAN_POINT('Ctrl Pts',(-0.548430926173578,-2.46117792359562,
4.10252187729233));
#6323=CARTESIAN_POINT('Ctrl Pts',(0.260984773772587,-2.64154221085939,4.15518293237521));
#6324=CARTESIAN_POINT('Ctrl Pts',(1.16807353539669,-2.38358186759794,4.20784398745809));
#6325=CARTESIAN_POINT('Ctrl Pts',(1.76145512481594,-1.8042863119436,4.26050504254097));
#6326=CARTESIAN_POINT('Ctrl Pts',(2.35483671423518,-1.22499075628926,4.31316609762385));
#6327=CARTESIAN_POINT('Ctrl Pts',(2.63451113144957,-0.32435998824203,4.36582715270673));
#6328=CARTESIAN_POINT('Ctrl Pts',(2.47364125533363,0.489154568739605,4.41848820778961));
#6329=CARTESIAN_POINT('Ctrl Pts',(2.31277137921768,1.30266912572123,4.47114926287248));
#6330=CARTESIAN_POINT('Ctrl Pts',(1.71135720977141,2.02906747163727,4.52381031795536));
#6331=CARTESIAN_POINT('Ctrl Pts',(0.942150336599642,2.33891555974628,4.57647137303824));
#6332=CARTESIAN_POINT('Ctrl Pts',(0.172943463427865,2.64876364785529,4.62913242812111));
#6333=CARTESIAN_POINT('Ctrl Pts',(-0.764056113469408,2.54206147815727,4.68179348320399));
#6334=CARTESIAN_POINT('Ctrl Pts',(-1.44390309505201,2.06720030576578,4.73445453828687));
#6335=CARTESIAN_POINT('Ctrl Pts',(-2.10214324411594,1.60743112627774,4.78544192469392));
#6336=CARTESIAN_POINT('Ctrl Pts',(-2.51931664968783,0.802532659807444,4.83642931110097));
#6337=CARTESIAN_POINT('Ctrl Pts',(-2.52142713785251,-0.000477745744092403,
4.88741669750802));
#6338=CARTESIAN_POINT('Origin',(0.,0.,0.));
#6339=CARTESIAN_POINT('',(-2.51595242716893,0.00210630723253068,5.88741669750802));
#6340=CARTESIAN_POINT('',(-2.51351075839737,-0.000354205898239757,5.61258330249198));
#6341=CARTESIAN_POINT('',(-2.5175,-3.08304831685346E-16,0.));
#6342=CARTESIAN_POINT('Ctrl Pts',(-2.51351075839737,-0.000354205898239757,
5.61258330249198));
#6343=CARTESIAN_POINT('Ctrl Pts',(-2.51295240495751,0.439819286417837,5.58485912956205));
#6344=CARTESIAN_POINT('Ctrl Pts',(-2.40289969386439,0.880253950489353,5.55713495663213));
#6345=CARTESIAN_POINT('Ctrl Pts',(-2.18499186098815,1.25856365282659,5.5294107837022));
#6346=CARTESIAN_POINT('Ctrl Pts',(-1.77108388187219,1.97714913140962,5.47674972861932));
#6347=CARTESIAN_POINT('Ctrl Pts',(-0.968038758408038,2.47159012985723,5.42408867353645));
#6348=CARTESIAN_POINT('Ctrl Pts',(-0.14005115833078,2.51764921624498,5.37142761845357));
#6349=CARTESIAN_POINT('Ctrl Pts',(0.687936441746484,2.56370830263272,5.3187665633707));
#6350=CARTESIAN_POINT('Ctrl Pts',(1.54086651843685,2.16138547696059,5.26610550828782));
#6351=CARTESIAN_POINT('Ctrl Pts',(2.03192072549116,1.49314100724674,5.21344445320494));
#6352=CARTESIAN_POINT('Ctrl Pts',(2.52297493254547,0.82489653753288,5.16078339812206));
#6353=CARTESIAN_POINT('Ctrl Pts',(2.65215326996372,-0.109269576222705,5.10812234303918));
#6354=CARTESIAN_POINT('Ctrl Pts',(2.36087115731916,-0.885697059154641,5.0554612879563));
#6355=CARTESIAN_POINT('Ctrl Pts',(2.0695890446746,-1.66212454208657,5.00280023287342));
#6356=CARTESIAN_POINT('Ctrl Pts',(1.35784648196724,-2.28081339419485,4.95013917779055));
#6357=CARTESIAN_POINT('Ctrl Pts',(0.548430867950845,-2.46117766231084,4.89747812270767));
#6358=CARTESIAN_POINT('Ctrl Pts',(-0.260984746065556,-2.64154193042683,
4.84481706762479));
#6359=CARTESIAN_POINT('Ctrl Pts',(-1.16807341139099,-2.38358161455052,4.79215601254191));
#6360=CARTESIAN_POINT('Ctrl Pts',(-1.76145493781535,-1.80428612039566,4.73949495745903));
#6361=CARTESIAN_POINT('Ctrl Pts',(-2.23813250929503,-1.33892419551938,4.69719107247001));
#6362=CARTESIAN_POINT('Ctrl Pts',(-2.5123656680334,-0.666195260483231,4.65488718748099));
#6363=CARTESIAN_POINT('Ctrl Pts',(-2.5184009829045,0.00215602902869219,
4.61258330249198));
#6364=CARTESIAN_POINT('Ctrl Pts',(-2.52142713785251,-0.000477745744092403,
4.88741669750802));
#6365=CARTESIAN_POINT('Ctrl Pts',(-2.52149641494594,-0.0268366838431701,
4.88909036618385));
#6366=CARTESIAN_POINT('Ctrl Pts',(-2.52111846566354,-0.0531935875744284,
4.89076403485968));
#6367=CARTESIAN_POINT('Ctrl Pts',(-2.52028713597104,-0.0795361833539025,
4.89243770353551));
#6368=CARTESIAN_POINT('Ctrl Pts',(-2.49412980903954,-0.9083913249971,4.94509875861839));
#6369=CARTESIAN_POINT('Ctrl Pts',(-2.01912076890865,-1.72308143319855,4.99775981370126));
#6370=CARTESIAN_POINT('Ctrl Pts',(-1.31068472178129,-2.15413063974552,5.05042086878414));
#6371=CARTESIAN_POINT('Ctrl Pts',(-0.602248674653905,-2.58517984629251,
5.10308192386702));
#6372=CARTESIAN_POINT('Ctrl Pts',(0.339614379469953,-2.632588151185,5.15574297894989));
#6373=CARTESIAN_POINT('Ctrl Pts',(1.08775347157826,-2.27485508019369,5.20840403403277));
#6374=CARTESIAN_POINT('Ctrl Pts',(1.83589256368657,-1.91712200920239,5.26106508911565));
#6375=CARTESIAN_POINT('Ctrl Pts',(2.39030769377933,-1.1542475623273,5.31372614419854));
#6376=CARTESIAN_POINT('Ctrl Pts',(2.49956213879293,-0.332208318368038,5.36638719928141));
#6377=CARTESIAN_POINT('Ctrl Pts',(2.60881658380653,0.489830925591221,5.4190482543643));
#6378=CARTESIAN_POINT('Ctrl Pts',(2.27291034374099,1.37103496663465,5.47170930944717));
#6379=CARTESIAN_POINT('Ctrl Pts',(1.64418263083336,1.91176272938481,5.52437036453004));
#6380=CARTESIAN_POINT('Ctrl Pts',(1.01545491792572,2.45249049213496,5.57703141961292));
#6381=CARTESIAN_POINT('Ctrl Pts',(0.0939057321760005,2.65274197659184,5.6296924746958));
#6382=CARTESIAN_POINT('Ctrl Pts',(-0.70252664300866,2.42169972484316,5.68235352977868));
#6383=CARTESIAN_POINT('Ctrl Pts',(-1.49895901819332,2.19065747309447,5.73501458486156));
#6384=CARTESIAN_POINT('Ctrl Pts',(-2.17027458281292,1.52832148514024,5.78767563994444));
#6385=CARTESIAN_POINT('Ctrl Pts',(-2.41202027244453,0.735072420070988,5.84033669502731));
#6386=CARTESIAN_POINT('Ctrl Pts',(-2.48406204758965,0.498679080992718,5.85603002918755));
#6387=CARTESIAN_POINT('Ctrl Pts',(-2.51795464778859,0.250659633631731,5.87172336334778));
#6388=CARTESIAN_POINT('Ctrl Pts',(-2.51595242716893,0.00210630723253068,
5.88741669750802));
#6389=CARTESIAN_POINT('Origin',(0.,0.,0.));
#6390=CARTESIAN_POINT('',(-2.51451849661665,-0.00155877597875643,6.88741669750802));
#6391=CARTESIAN_POINT('',(-2.51965512385738,-0.00182887343565974,6.61258330249198));
#6392=CARTESIAN_POINT('',(-2.5175,-3.08304831685346E-16,0.));
#6393=CARTESIAN_POINT('Ctrl Pts',(-2.51965512385738,-0.00182887343565974,
6.61258330249198));
#6394=CARTESIAN_POINT('Ctrl Pts',(-2.51382586072417,0.70963927099582,6.56749212672599));
#6395=CARTESIAN_POINT('Ctrl Pts',(-2.19770441709654,1.42564242834162,6.52240095096));
#6396=CARTESIAN_POINT('Ctrl Pts',(-1.66427222622564,1.89429928459087,6.47730977519401));
#6397=CARTESIAN_POINT('Ctrl Pts',(-1.04128776176594,2.44163397042813,6.42464872011113));
#6398=CARTESIAN_POINT('Ctrl Pts',(-0.121903980861276,2.65160257796401,6.37198766502826));
#6399=CARTESIAN_POINT('Ctrl Pts',(0.676922910116403,2.4289807131762,6.31932660994538));
#6400=CARTESIAN_POINT('Ctrl Pts',(1.47574980109409,2.20635884838837,6.2666655548625));
#6401=CARTESIAN_POINT('Ctrl Pts',(2.15401980214479,1.55114651127684,6.21400449977962));
#6402=CARTESIAN_POINT('Ctrl Pts',(2.40412587747264,0.760493703272659,6.16134344469674));
#6403=CARTESIAN_POINT('Ctrl Pts',(2.65423195280049,-0.0301591047315269,
6.10868238961386));
#6404=CARTESIAN_POINT('Ctrl Pts',(2.47617410240549,-0.956252383628369,6.05602133453099));
#6405=CARTESIAN_POINT('Ctrl Pts',(1.95070460798478,-1.59778703954676,6.00336027944811));
#6406=CARTESIAN_POINT('Ctrl Pts',(1.42523511356408,-2.23932169546514,5.95069922436523));
#6407=CARTESIAN_POINT('Ctrl Pts',(0.552353975117676,-2.59629772840507,5.89803816928235));
#6408=CARTESIAN_POINT('Ctrl Pts',(-0.272072318490672,-2.50682040851643,
5.84537711419947));
#6409=CARTESIAN_POINT('Ctrl Pts',(-1.09649861209903,-2.4173430886278,5.79271605911659));
#6410=CARTESIAN_POINT('Ctrl Pts',(-1.87247006086932,-1.88141241591059,5.74005500403372));
#6411=CARTESIAN_POINT('Ctrl Pts',(-2.24807036787059,-1.14208210019275,5.68739394895084));
#6412=CARTESIAN_POINT('Ctrl Pts',(-2.42593046918386,-0.791982905899236,
5.66245706679789));
#6413=CARTESIAN_POINT('Ctrl Pts',(-2.5140129769474,-0.396274204395027,5.63752018464493));
#6414=CARTESIAN_POINT('Ctrl Pts',(-2.51351075839737,-0.000354205898239757,
5.61258330249198));
#6415=CARTESIAN_POINT('Ctrl Pts',(-2.51595242716893,0.00210630723253068,
5.88741669750802));
#6416=CARTESIAN_POINT('Ctrl Pts',(-2.51123593210567,-0.583393874621885,
5.92438441843066));
#6417=CARTESIAN_POINT('Ctrl Pts',(-2.30733899175125,-1.17185655251717,5.9613521393533));
#6418=CARTESIAN_POINT('Ctrl Pts',(-1.93372918822543,-1.61829067462528,5.99831986027594));
#6419=CARTESIAN_POINT('Ctrl Pts',(-1.40151659973107,-2.25424256206805,6.05098091535882));
#6420=CARTESIAN_POINT('Ctrl Pts',(-0.524915608098723,-2.60198419476933,
6.1036419704417));
#6421=CARTESIAN_POINT('Ctrl Pts',(0.298520273710652,-2.50380886237859,6.15630302552458));
#6422=CARTESIAN_POINT('Ctrl Pts',(1.12195615552003,-2.40563352998785,6.20896408060746));
#6423=CARTESIAN_POINT('Ctrl Pts',(1.89222692750642,-1.8615412325051,6.26162513569033));
#6424=CARTESIAN_POINT('Ctrl Pts',(2.26000165505001,-1.11828700772708,6.31428619077321));
#6425=CARTESIAN_POINT('Ctrl Pts',(2.62777638259361,-0.375032782949049,6.36694724585609));
#6426=CARTESIAN_POINT('Ctrl Pts',(2.59305506569438,0.567383369124259,6.41960830093898));
#6427=CARTESIAN_POINT('Ctrl Pts',(2.17158440269112,1.28155943991538,6.47226935602186));
#6428=CARTESIAN_POINT('Ctrl Pts',(1.75011373968786,1.99573551070649,6.52493041110473));
#6429=CARTESIAN_POINT('Ctrl Pts',(0.941893730580582,2.48167150021543,6.57759146618761));
#6430=CARTESIAN_POINT('Ctrl Pts',(0.11346596452102,2.51898752751594,6.63025252127048));
#6431=CARTESIAN_POINT('Ctrl Pts',(-0.714961801538553,2.55630355481645,6.68291357635336));
#6432=CARTESIAN_POINT('Ctrl Pts',(-1.56359732455041,2.14499961990851,6.73557463143624));
#6433=CARTESIAN_POINT('Ctrl Pts',(-2.04756995383571,1.47160834288076,6.78823568651912));
#6434=CARTESIAN_POINT('Ctrl Pts',(-2.35140545800432,1.04885679500788,6.82129602351542));
#6435=CARTESIAN_POINT('Ctrl Pts',(-2.51151771720726,0.522809727020648,6.85435636051172));
#6436=CARTESIAN_POINT('Ctrl Pts',(-2.51451849661665,-0.00155877597875643,
6.88741669750802));
#6437=CARTESIAN_POINT('Origin',(0.,0.,0.));
#6438=CARTESIAN_POINT('',(-2.52134266056864,-0.000655147898209446,7.88741669750802));
#6439=CARTESIAN_POINT('',(-2.5186623288877,0.00210982157644382,7.61258330249198));
#6440=CARTESIAN_POINT('',(-2.5175,-3.08304831685346E-16,0.));
#6441=CARTESIAN_POINT('Ctrl Pts',(-2.5186623288877,0.00210982157644382,
7.61258330249198));
#6442=CARTESIAN_POINT('Ctrl Pts',(-2.52004665861774,0.156851743540232,7.6027861789728));
#6443=CARTESIAN_POINT('Ctrl Pts',(-2.50699659804811,0.311360834758803,7.59298905545363));
#6444=CARTESIAN_POINT('Ctrl Pts',(-2.4786676666043,0.463015723985691,7.58319193193445));
#6445=CARTESIAN_POINT('Ctrl Pts',(-2.32639527601114,1.27818422314105,7.53053087685157));
#6446=CARTESIAN_POINT('Ctrl Pts',(-1.73268133779952,2.01088829447311,7.47786982176869));
#6447=CARTESIAN_POINT('Ctrl Pts',(-0.966787934844472,2.32883856578358,7.42520876668581));
#6448=CARTESIAN_POINT('Ctrl Pts',(-0.200894531889431,2.64678883709404,7.37254771160294));
#6449=CARTESIAN_POINT('Ctrl Pts',(0.737178335809047,2.54998530838289,7.31988665652006));
#6450=CARTESIAN_POINT('Ctrl Pts',(1.4220000139359,2.08232771749063,7.26722560143718));
#6451=CARTESIAN_POINT('Ctrl Pts',(2.10682169206276,1.61467012659837,7.2145645463543));
#6452=CARTESIAN_POINT('Ctrl Pts',(2.53839218061801,0.776158473525024,7.16190349127142));
#6453=CARTESIAN_POINT('Ctrl Pts',(2.52098616593426,-0.0529266873392757,
7.10924243618854));
#6454=CARTESIAN_POINT('Ctrl Pts',(2.5035801512505,-0.882011848203581,7.05658138110567));
#6455=CARTESIAN_POINT('Ctrl Pts',(2.03719763332772,-1.70167051685883,7.00392032602279));
#6456=CARTESIAN_POINT('Ctrl Pts',(1.33335142587202,-2.14017413090131,6.95125927093991));
#6457=CARTESIAN_POINT('Ctrl Pts',(0.629505218416328,-2.57867774494379,6.89859821585704));
#6458=CARTESIAN_POINT('Ctrl Pts',(-0.31180467857228,-2.63602630437352,6.84593716077416));
#6459=CARTESIAN_POINT('Ctrl Pts',(-1.0636783622589,-2.28621092837513,6.79327610569128));
#6460=CARTESIAN_POINT('Ctrl Pts',(-1.81555204594553,-1.93639555237673,6.7406150506084));
#6461=CARTESIAN_POINT('Ctrl Pts',(-2.37798951633018,-1.17941624095021,6.68795399552552));
#6462=CARTESIAN_POINT('Ctrl Pts',(-2.49591567751513,-0.358576203167625,
6.63529294044265));
#6463=CARTESIAN_POINT('Ctrl Pts',(-2.51286723321544,-0.240582744534753,
6.62772306112576));
#6464=CARTESIAN_POINT('Ctrl Pts',(-2.5206337370267,-0.121269715233796,6.62015318180887));
#6465=CARTESIAN_POINT('Ctrl Pts',(-2.51965512385738,-0.00182887343565974,
6.61258330249198));
#6466=CARTESIAN_POINT('Ctrl Pts',(-2.51451849661665,-0.00155877597875643,
6.88741669750802));
#6467=CARTESIAN_POINT('Ctrl Pts',(-2.51629759013436,-0.312444874989867,
6.9070174155946));
#6468=CARTESIAN_POINT('Ctrl Pts',(-2.4628514793145,-0.622740952860776,6.92661813368118));
#6469=CARTESIAN_POINT('Ctrl Pts',(-2.35139007912217,-0.910570591403298,
6.94621885176775));
#6470=CARTESIAN_POINT('Ctrl Pts',(-2.0519278395646,-1.68387962951205,6.99887990685063));
#6471=CARTESIAN_POINT('Ctrl Pts',(-1.33369362489071,-2.295019086582,7.05154096193351));
#6472=CARTESIAN_POINT('Ctrl Pts',(-0.522419062335059,-2.46682947727924,
7.10420201701639));
#6473=CARTESIAN_POINT('Ctrl Pts',(0.288855500220588,-2.63863986797649,7.15686307209927));
#6474=CARTESIAN_POINT('Ctrl Pts',(1.193170410658,-2.37112119230105,7.20952412718215));
#6475=CARTESIAN_POINT('Ctrl Pts',(1.78040371769394,-1.78559258972849,7.26218518226502));
#6476=CARTESIAN_POINT('Ctrl Pts',(2.36763702472988,-1.20006398715593,7.3148462373479));
#6477=CARTESIAN_POINT('Ctrl Pts',(2.63778872836434,-0.296525457686245,7.36750729243078));
#6478=CARTESIAN_POINT('Ctrl Pts',(2.4683398583974,0.515243006912746,7.42016834751366));
#6479=CARTESIAN_POINT('Ctrl Pts',(2.29889098843046,1.32701147151174,7.47282940259653));
#6480=CARTESIAN_POINT('Ctrl Pts',(1.68984154486212,2.04700987124004,7.52549045767942));
#6481=CARTESIAN_POINT('Ctrl Pts',(0.917406920482627,2.34872549572162,7.57815151276229));
#6482=CARTESIAN_POINT('Ctrl Pts',(0.144972296103131,2.6504411202032,7.63081256784517));
#6483=CARTESIAN_POINT('Ctrl Pts',(-0.790847509087517,2.53387396943805,7.68347362292805));
#6484=CARTESIAN_POINT('Ctrl Pts',(-1.46564430234878,2.05185315227782,7.73613467801093));
#6485=CARTESIAN_POINT('Ctrl Pts',(-2.11181835180565,1.59027813227568,7.78656201784329));
#6486=CARTESIAN_POINT('Ctrl Pts',(-2.51864329962567,0.793594701352211,7.83698935767566));
#6487=CARTESIAN_POINT('Ctrl Pts',(-2.52134266056864,-0.000655147898209446,
7.88741669750802));
#6488=CARTESIAN_POINT('Origin',(0.,0.,0.));
#6489=CARTESIAN_POINT('',(-2.51592828109546,0.00320694493696498,8.88741669750802));
#6490=CARTESIAN_POINT('',(-2.51342302570288,-0.000307789261743824,8.61258330249198));
#6491=CARTESIAN_POINT('',(-2.5175,-3.08304831685346E-16,0.));
#6492=CARTESIAN_POINT('',(-1.91346599666506,-1.63598720337495,9.));
#6493=CARTESIAN_POINT('Ctrl Pts',(-2.51592828109546,0.00320694493696498,
8.88741669750802));
#6494=CARTESIAN_POINT('Ctrl Pts',(-2.51065601785214,-0.589289396470771,
8.92494446500535));
#6495=CARTESIAN_POINT('Ctrl Pts',(-2.29922182808405,-1.18480356030443,8.96247223250267));
#6496=CARTESIAN_POINT('Ctrl Pts',(-1.91346599666504,-1.63598720337498,9.));
#6497=CARTESIAN_POINT('',(1.91703628304852,-1.63862073901331,9.));
#6498=CARTESIAN_POINT('Origin',(0.,0.,9.));
#6499=CARTESIAN_POINT('Ctrl Pts',(1.91704088636911,-1.63862413454171,9.));
#6500=CARTESIAN_POINT('Ctrl Pts',(1.39386644228135,-2.2478675793879,8.94901908464117));
#6501=CARTESIAN_POINT('Ctrl Pts',(0.553382875999586,-2.58772269472312,8.89803816928235));
#6502=CARTESIAN_POINT('Ctrl Pts',(-0.245732947937194,-2.50932486329663,
8.84705725392353));
#6503=CARTESIAN_POINT('Ctrl Pts',(-1.0711846316848,-2.42834333344235,8.79439619884064));
#6504=CARTESIAN_POINT('Ctrl Pts',(-1.85249699178243,-1.90108649006683,8.74173514375777));
#6505=CARTESIAN_POINT('Ctrl Pts',(-2.23581570064333,-1.16587069267918,8.68907408867489));
#6506=CARTESIAN_POINT('Ctrl Pts',(-2.42140730689609,-0.80990090141839,8.66357715994725));
#6507=CARTESIAN_POINT('Ctrl Pts',(-2.51370081905187,-0.40518115145991,8.63808023121962));
#6508=CARTESIAN_POINT('Ctrl Pts',(-2.51342302570288,-0.000307789261743824,
8.61258330249198));
#6509=CARTESIAN_POINT('Origin',(0.,0.,-2.20842344717745));
#6510=CARTESIAN_POINT('',(-3.07819132760982,-0.00079983994656474,8.20842344717746));
#6511=CARTESIAN_POINT('',(-3.0685226095324,-0.00037576575812523,8.29157655282255));
#6512=CARTESIAN_POINT('',(-3.0735,-1.43456032168185E-13,-2.20842344717745));
#6513=CARTESIAN_POINT('',(0.793799282532882,2.96922295374569,9.));
#6514=CARTESIAN_POINT('Ctrl Pts',(-3.0685226095324,-0.000375765758125098,
8.29157655282255));
#6515=CARTESIAN_POINT('Ctrl Pts',(-3.06886175465975,-0.494667038336489,
8.31707348155019));
#6516=CARTESIAN_POINT('Ctrl Pts',(-2.72346330097092,-2.00928678297278,8.39523146536071));
#6517=CARTESIAN_POINT('Ctrl Pts',(-0.353891728589143,-3.60835636284,8.52605050425409));
#6518=CARTESIAN_POINT('Ctrl Pts',(2.83103930764092,-2.27044520800339,8.68403366950274));
#6519=CARTESIAN_POINT('Ctrl Pts',(3.44352590057726,1.13463251498715,8.84201683475136));
#6520=CARTESIAN_POINT('Ctrl Pts',(1.77625330176034,2.70657130793361,8.94733894491712));
#6521=CARTESIAN_POINT('Ctrl Pts',(0.793799282532882,2.96922295374569,9.));
#6522=CARTESIAN_POINT('',(-0.793799282532857,2.9692229537457,9.));
#6523=CARTESIAN_POINT('Origin',(0.,0.,9.));
#6524=CARTESIAN_POINT('Ctrl Pts',(-3.07819132760982,-0.000799839946564419,
8.20842344717746));
#6525=CARTESIAN_POINT('Ctrl Pts',(-3.07833730528696,-0.0437517646857214,
8.21065716242797));
#6526=CARTESIAN_POINT('Ctrl Pts',(-3.05813411202838,-1.09917547321831,8.26555193276136));
#6527=CARTESIAN_POINT('Ctrl Pts',(-1.85231323033622,-3.11779603581512,8.37310775817763));
#6528=CARTESIAN_POINT('Ctrl Pts',(1.59892942568934,-3.25553164520284,8.53109092342626));
#6529=CARTESIAN_POINT('Ctrl Pts',(3.59995819558759,-0.439170790472673,8.68907408867489));
#6530=CARTESIAN_POINT('Ctrl Pts',(2.34901404634718,2.73903334879023,8.84537711419948));
#6531=CARTESIAN_POINT('Ctrl Pts',(0.15211409622113,3.22551487048637,8.94901908464117));
#6532=CARTESIAN_POINT('Ctrl Pts',(-0.795573338178512,2.9743476420004,8.99999999999999));
#6533=CARTESIAN_POINT('Origin',(0.,0.,-2.20842344717745));
#6534=CARTESIAN_POINT('',(-3.06986001960329,-0.00190303792297591,7.20842344717746));
#6535=CARTESIAN_POINT('',(-3.07491903389726,0.00257578415689406,7.29157655282255));
#6536=CARTESIAN_POINT('',(-3.0735,-1.43456032168185E-13,-2.20842344717745));
#6537=CARTESIAN_POINT('Ctrl Pts',(-3.07491903389726,0.00257578415689394,
7.29157655282255));
#6538=CARTESIAN_POINT('Ctrl Pts',(-3.06752474008062,-0.823966629777171,
7.33444048438625));
#6539=CARTESIAN_POINT('Ctrl Pts',(-2.2992951061863,-2.67809470862681,7.42996547103282));
#6540=CARTESIAN_POINT('Ctrl Pts',(0.826109632836259,-3.5313227329181,7.57815151276229));
#6541=CARTESIAN_POINT('Ctrl Pts',(3.40888391949913,-1.23800854484421,7.73613467801092));
#6542=CARTESIAN_POINT('Ctrl Pts',(2.89959383691459,2.17837089371843,7.89411784325955));
#6543=CARTESIAN_POINT('Ctrl Pts',(-0.239554039779309,3.61860800891848,8.0521010085082));
#6544=CARTESIAN_POINT('Ctrl Pts',(-2.69013535674363,2.07437726859049,8.18458724502919));
#6545=CARTESIAN_POINT('Ctrl Pts',(-3.06816128832425,0.526236310858699,8.26441242646731));
#6546=CARTESIAN_POINT('Ctrl Pts',(-3.0685226095324,-0.000375765758125098,
8.29157655282255));
#6547=CARTESIAN_POINT('Ctrl Pts',(-3.06986001960329,-0.00190303792297591,
7.20842344717746));
#6548=CARTESIAN_POINT('Ctrl Pts',(-3.07203203307961,-0.381449582236985,
7.22802416526404));
#6549=CARTESIAN_POINT('Ctrl Pts',(-2.83147587564289,-1.7780644343801,7.30028593843349));
#6550=CARTESIAN_POINT('Ctrl Pts',(-0.751386096246847,-3.5479953461427,7.42520876668581));
#6551=CARTESIAN_POINT('Ctrl Pts',(2.56072339002455,-2.56819159278999,7.58319193193446));
#6552=CARTESIAN_POINT('Ctrl Pts',(3.55017077169744,0.741074350000556,7.74117509718308));
#6553=CARTESIAN_POINT('Ctrl Pts',(1.31948938364505,3.37811317609581,7.89915826243173));
#6554=CARTESIAN_POINT('Ctrl Pts',(-2.05954752837555,2.95721515386999,8.05490771242984));
#6555=CARTESIAN_POINT('Ctrl Pts',(-3.07489580194622,0.968863282862285,8.1579961073451));
#6556=CARTESIAN_POINT('Ctrl Pts',(-3.07819132760982,-0.000799839946564419,
8.20842344717746));
#6557=CARTESIAN_POINT('Origin',(0.,0.,-2.20842344717745));
#6558=CARTESIAN_POINT('',(-3.07161063948509,0.00257149365592749,6.20842344717746));
#6559=CARTESIAN_POINT('',(-3.07613109162886,-0.00223278748941785,6.29157655282255));
#6560=CARTESIAN_POINT('',(-3.0735,-1.43456032168185E-13,-2.20842344717745));
#6561=CARTESIAN_POINT('Ctrl Pts',(-3.07613109162887,-0.00223278748941807,
6.29157655282255));
#6562=CARTESIAN_POINT('Ctrl Pts',(-3.07732583545246,-0.148052619571458,
6.29914643213944));
#6563=CARTESIAN_POINT('Ctrl Pts',(-3.00188266295528,-1.30704946930654,6.3593773665392));
#6564=CARTESIAN_POINT('Ctrl Pts',(-1.5298699694087,-3.288217534816,6.47226935602186));
#6565=CARTESIAN_POINT('Ctrl Pts',(1.91773595122029,-3.07817487653525,6.63025252127048));
#6566=CARTESIAN_POINT('Ctrl Pts',(3.62589086939586,-0.0761241300265441,
6.78823568651912));
#6567=CARTESIAN_POINT('Ctrl Pts',(2.04523716940625,2.99497684203422,6.94621885176775));
#6568=CARTESIAN_POINT('Ctrl Pts',(-1.39051293053958,3.34952577410217,7.10420201701639));
#6569=CARTESIAN_POINT('Ctrl Pts',(-2.97503873711316,1.39405793869258,7.21932125070132));
#6570=CARTESIAN_POINT('Ctrl Pts',(-3.07660909841575,0.191493081934767,7.28177942930337));
#6571=CARTESIAN_POINT('Ctrl Pts',(-3.07491903389726,0.00257578415689394,
7.29157655282255));
#6572=CARTESIAN_POINT('Ctrl Pts',(-3.07161063948509,0.00257149365592728,
6.20842344717746));
#6573=CARTESIAN_POINT('Ctrl Pts',(-3.06585248751805,-0.712238758153184,
6.2453911681001));
#6574=CARTESIAN_POINT('Ctrl Pts',(-2.46232196902915,-2.45407551393839,6.33501994410562));
#6575=CARTESIAN_POINT('Ctrl Pts',(0.429356514911867,-3.60118463981366,6.47730977519402));
#6576=CARTESIAN_POINT('Ctrl Pts',(3.25052102458439,-1.60841283090018,6.63529294044265));
#6577=CARTESIAN_POINT('Ctrl Pts',(3.12335204644367,1.8432448176368,6.79327610569127));
#6578=CARTESIAN_POINT('Ctrl Pts',(0.163196100475927,3.6230155390935,6.95125927093992));
#6579=CARTESIAN_POINT('Ctrl Pts',(-2.55935722897219,2.3034892324118,7.08964171810198));
#6580=CARTESIAN_POINT('Ctrl Pts',(-3.06619650599269,0.638274357893825,7.17536311018116));
#6581=CARTESIAN_POINT('Ctrl Pts',(-3.06986001960329,-0.00190303792297591,
7.20842344717746));
#6582=CARTESIAN_POINT('Origin',(0.,0.,-2.20842344717745));
#6583=CARTESIAN_POINT('',(-3.07829446204158,-0.000583257813248639,5.20842344717746));
#6584=CARTESIAN_POINT('',(-3.06862971834531,-0.000432433695449898,5.29157655282255));
#6585=CARTESIAN_POINT('',(-3.0735,-1.43456032168185E-13,-2.20842344717745));
#6586=CARTESIAN_POINT('Ctrl Pts',(-3.06862971834531,-0.000432433695450388,
5.29157655282255));
#6587=CARTESIAN_POINT('Ctrl Pts',(-3.06924285388195,-0.483792956189932,
5.3165134349755));
#6588=CARTESIAN_POINT('Ctrl Pts',(-2.73461550492184,-1.98709885774611,5.39411137221133));
#6589=CARTESIAN_POINT('Ctrl Pts',(-0.391316876461119,-3.60551614915347,
5.52437036453005));
#6590=CARTESIAN_POINT('Ctrl Pts',(2.80566446893912,-2.29806927260028,5.68235352977867));
#6591=CARTESIAN_POINT('Ctrl Pts',(3.45781239726766,1.09380483983996,5.84033669502732));
#6592=CARTESIAN_POINT('Ctrl Pts',(0.97360642122477,3.49356069061924,5.99831986027594));
#6593=CARTESIAN_POINT('Ctrl Pts',(-2.23234707976449,2.76138593791136,6.1487331462077));
#6594=CARTESIAN_POINT('Ctrl Pts',(-3.06901441228829,0.866365958055841,6.24648537705656));
#6595=CARTESIAN_POINT('Ctrl Pts',(-3.07613109162887,-0.00223278748941807,
6.29157655282255));
#6596=CARTESIAN_POINT('Ctrl Pts',(-3.07829446204158,-0.000583257813248778,
5.20842344717746));
#6597=CARTESIAN_POINT('Ctrl Pts',(-3.07837903925972,-0.0327636734030677,
5.21009711585329));
#6598=CARTESIAN_POINT('Ctrl Pts',(-3.06339926603453,-1.07740235694415,5.26443183961199));
#6599=CARTESIAN_POINT('Ctrl Pts',(-1.88513501425953,-3.09824859284726,5.37142761845357));
#6600=CARTESIAN_POINT('Ctrl Pts',(1.56449687870927,-3.27188445193808,5.52941078370221));
#6601=CARTESIAN_POINT('Ctrl Pts',(3.59507670274909,-0.477809442042676,5.68739394895084));
#6602=CARTESIAN_POINT('Ctrl Pts',(2.36479925030647,2.74965505068462,5.84537711419948));
#6603=CARTESIAN_POINT('Ctrl Pts',(-1.01043183895086,3.48308854122473,6.00336027944811));
#6604=CARTESIAN_POINT('Ctrl Pts',(-2.89382807597609,1.62488477968039,6.1243757237741));
#6605=CARTESIAN_POINT('Ctrl Pts',(-3.07405505858123,0.306018821833909,6.19273011301722));
#6606=CARTESIAN_POINT('Ctrl Pts',(-3.07161063948509,0.00257149365592728,
6.20842344717746));
#6607=CARTESIAN_POINT('Origin',(0.,0.,-2.20842344717745));
#6608=CARTESIAN_POINT('',(-3.07007340747988,-0.00202528632500865,4.20842344717746));
#6609=CARTESIAN_POINT('',(-3.07459996860257,0.00263219671087622,4.29157655282255));
#6610=CARTESIAN_POINT('',(-3.0735,-1.43456032168185E-13,-2.20842344717745));
#6611=CARTESIAN_POINT('Ctrl Pts',(-3.07459996860257,0.00263219671087611,
4.29157655282254));
#6612=CARTESIAN_POINT('Ctrl Pts',(-3.06723173016907,-0.813327163096425,
4.33388043781156));
#6613=CARTESIAN_POINT('Ctrl Pts',(-2.31566637879303,-2.65701288209306,4.42884537788346));
#6614=CARTESIAN_POINT('Ctrl Pts',(0.788798568359572,-3.5398689787538,4.57647137303824));
#6615=CARTESIAN_POINT('Ctrl Pts',(3.39559987896266,-1.27388265864876,4.73445453828687));
#6616=CARTESIAN_POINT('Ctrl Pts',(2.92247620064489,2.14755871250649,4.8924377035355));
#6617=CARTESIAN_POINT('Ctrl Pts',(-0.201433142800403,3.62109103191458,5.05042086878414));
#6618=CARTESIAN_POINT('Ctrl Pts',(-2.6783810755718,2.0960153254597,5.18346715187982));
#6619=CARTESIAN_POINT('Ctrl Pts',(-3.06794805030265,0.53695514470911,5.26385237989262));
#6620=CARTESIAN_POINT('Ctrl Pts',(-3.06862971834531,-0.000432433695450388,
5.29157655282255));
#6621=CARTESIAN_POINT('Ctrl Pts',(-3.07007340747988,-0.00202528632500865,
4.20842344717746));
#6622=CARTESIAN_POINT('Ctrl Pts',(-3.0723295005003,-0.370662586915465,4.22746411868935));
#6623=CARTESIAN_POINT('Ctrl Pts',(-2.84084702177449,-1.75610719556142,4.29916584528412));
#6624=CARTESIAN_POINT('Ctrl Pts',(-0.788798652099944,-3.53986935455429,
4.42352862696176));
#6625=CARTESIAN_POINT('Ctrl Pts',(2.53347023630324,-2.59507358691089,4.5815117922104));
#6626=CARTESIAN_POINT('Ctrl Pts',(3.55779514749501,0.703542499198116,4.73949495745903));
#6627=CARTESIAN_POINT('Ctrl Pts',(1.35507842480211,3.36402152542208,4.89747812270768));
#6628=CARTESIAN_POINT('Ctrl Pts',(-2.04038409747331,2.97735836442599,5.05378761928047));
#6629=CARTESIAN_POINT('Ctrl Pts',(-3.07571786407773,0.979775225389444,5.1574360607704));
#6630=CARTESIAN_POINT('Ctrl Pts',(-3.07829446204158,-0.000583257813248778,
5.20842344717746));
#6631=CARTESIAN_POINT('Origin',(0.,0.,-2.20842344717745));
#6632=CARTESIAN_POINT('',(-3.07132633130557,0.00250471562149607,3.20842344717745));
#6633=CARTESIAN_POINT('',(-3.07641449414843,-0.00211863766902523,3.29157655282255));
#6634=CARTESIAN_POINT('',(-3.0735,-1.43456032168185E-13,-2.20842344717745));
#6635=CARTESIAN_POINT('Ctrl Pts',(-3.07641449414843,-0.00211863766902543,
3.29157655282255));
#6636=CARTESIAN_POINT('Ctrl Pts',(-3.07748039759417,-0.137117714402335,
3.29858638556475));
#6637=CARTESIAN_POINT('Ctrl Pts',(-3.00831480734457,-1.28519241705506,3.35825727338983));
#6638=CARTESIAN_POINT('Ctrl Pts',(-1.56449671262057,-3.27188410457269,3.47058921629779));
#6639=CARTESIAN_POINT('Ctrl Pts',(1.88513481412996,-3.09824826393655,3.62857238154643));
#6640=CARTESIAN_POINT('Ctrl Pts',(3.6248847206042,-0.114395495228309,3.78655554679506));
#6641=CARTESIAN_POINT('Ctrl Pts',(2.07674046049821,2.97321789072832,3.9445387120437));
#6642=CARTESIAN_POINT('Ctrl Pts',(-1.35507828094373,3.36402116829015,4.10252187729233));
#6643=CARTESIAN_POINT('Ctrl Pts',(-2.96796315791591,1.41595115878974,4.21820115755195));
#6644=CARTESIAN_POINT('Ctrl Pts',(-3.07640391873074,0.202401789536568,4.28121938272868));
#6645=CARTESIAN_POINT('Ctrl Pts',(-3.07459996860257,0.00263219671087611,
4.29157655282254));
#6646=CARTESIAN_POINT('Ctrl Pts',(-3.07132633130557,0.00250471562149589,
3.20842344717745));
#6647=CARTESIAN_POINT('Ctrl Pts',(-3.06584026152828,-0.701641494300131,
3.24483112152541));
#6648=CARTESIAN_POINT('Ctrl Pts',(-2.47675782003803,-2.4325802671815,3.33389985095624));
#6649=CARTESIAN_POINT('Ctrl Pts',(0.39131691802336,-3.60551653188198,3.47562963546996));
#6650=CARTESIAN_POINT('Ctrl Pts',(3.23336081192176,-1.64263697190919,3.63361280071859));
#6651=CARTESIAN_POINT('Ctrl Pts',(3.14263608255428,1.81017037953698,3.79159596596722));
#6652=CARTESIAN_POINT('Ctrl Pts',(0.20143316418192,3.62109141633224,3.94957913121586));
#6653=CARTESIAN_POINT('Ctrl Pts',(-2.54597223044503,2.32515411521603,4.0885216249526));
#6654=CARTESIAN_POINT('Ctrl Pts',(-3.06608979205588,0.648882820391893,4.17480306360647));
#6655=CARTESIAN_POINT('Ctrl Pts',(-3.07007340747988,-0.00202528632500865,
4.20842344717746));
#6656=CARTESIAN_POINT('Origin',(0.,0.,-2.20842344717745));
#6657=CARTESIAN_POINT('',(-3.07837144959354,-0.000390310105172764,2.20842344717746));
#6658=CARTESIAN_POINT('',(-3.0686847313066,-0.00060378848225347,2.29157655282255));
#6659=CARTESIAN_POINT('',(-3.0735,-1.43456032168185E-13,-2.20842344717745));
#6660=CARTESIAN_POINT('Ctrl Pts',(-3.0686847313066,-0.000603788482253509,
2.29157655282255));
#6661=CARTESIAN_POINT('Ctrl Pts',(-3.06952252124188,-0.473087586699036,
2.31595338840081));
#6662=CARTESIAN_POINT('Ctrl Pts',(-2.7454388394421,-1.96518478392561,2.39299127906196));
#6663=CARTESIAN_POINT('Ctrl Pts',(-0.429356469436753,-3.60118425699533,
2.52269022480598));
#6664=CARTESIAN_POINT('Ctrl Pts',(2.78124872844843,-2.32755908045191,2.68067339005463));
#6665=CARTESIAN_POINT('Ctrl Pts',(3.46916639160829,1.05724176501438,2.83865655530325));
#6666=CARTESIAN_POINT('Ctrl Pts',(1.01043173169663,3.48308817136713,2.99663972055189));
#6667=CARTESIAN_POINT('Ctrl Pts',(-2.21503745439621,2.78219775503983,3.14761305305832));
#6668=CARTESIAN_POINT('Ctrl Pts',(-3.06947284561207,0.877056814069305,3.24592533048187));
#6669=CARTESIAN_POINT('Ctrl Pts',(-3.07641449414843,-0.00211863766902543,
3.29157655282255));
#6670=CARTESIAN_POINT('Ctrl Pts',(-3.07837144959354,-0.000390310105173098,
2.20842344717746));
#6671=CARTESIAN_POINT('Ctrl Pts',(-3.07841005815743,-0.021801014405184,
2.2095370692786));
#6672=CARTESIAN_POINT('Ctrl Pts',(-3.06854699220857,-1.05564638938531,2.26331174646262));
#6673=CARTESIAN_POINT('Ctrl Pts',(-1.9177361559176,-3.07817520619115,2.36974747872952));
#6674=CARTESIAN_POINT('Ctrl Pts',(1.52987013245233,-3.28821788231848,2.52773064397815));
#6675=CARTESIAN_POINT('Ctrl Pts',(3.58983249342927,-0.515733880008737,2.68571380922678));
#6676=CARTESIAN_POINT('Ctrl Pts',(2.39369399271082,2.72453792342614,2.84369697447542));
#6677=CARTESIAN_POINT('Ctrl Pts',(-0.973606524696896,3.49356106124283,3.00168013972405));
#6678=CARTESIAN_POINT('Ctrl Pts',(-2.88532029877192,1.64683564550024,3.12325563062473));
#6679=CARTESIAN_POINT('Ctrl Pts',(-3.073775462771,0.31685482580784,3.19217006644253));
#6680=CARTESIAN_POINT('Ctrl Pts',(-3.07132633130557,0.00250471562149589,
3.20842344717745));
#6681=CARTESIAN_POINT('Origin',(0.,0.,-2.20842344717745));
#6682=CARTESIAN_POINT('',(-3.07029648698129,-0.00213295581009409,1.20842344717745));
#6683=CARTESIAN_POINT('',(-3.07427865213087,0.00268124138861234,1.29157655282254));
#6684=CARTESIAN_POINT('',(-3.0735,-1.43456032168185E-13,-2.20842344717745));
#6685=CARTESIAN_POINT('Ctrl Pts',(-3.07427865213087,0.00268124138861233,
1.29157655282254));
#6686=CARTESIAN_POINT('Ctrl Pts',(-3.06696859167679,-0.802693165681438,
1.33332039123688));
#6687=CARTESIAN_POINT('Ctrl Pts',(-2.33184421030331,-2.63589937589878,1.42772528473409));
#6688=CARTESIAN_POINT('Ctrl Pts',(0.751386011701174,-3.5479949524756,1.57479123331418));
#6689=CARTESIAN_POINT('Ctrl Pts',(3.3819631285828,-1.30965902445964,1.73277439856281));
#6690=CARTESIAN_POINT('Ctrl Pts',(2.94498385958509,2.11658913035191,1.89075756381145));
#6691=CARTESIAN_POINT('Ctrl Pts',(-0.163196082436613,3.62301515147438,2.04874072906008));
#6692=CARTESIAN_POINT('Ctrl Pts',(-2.6665990793913,2.11786358985906,2.18234705873045));
#6693=CARTESIAN_POINT('Ctrl Pts',(-3.06771265130252,0.54761484384293,2.26329233331794));
#6694=CARTESIAN_POINT('Ctrl Pts',(-3.0686847313066,-0.000603788482253509,
2.29157655282255));
#6695=CARTESIAN_POINT('Ctrl Pts',(-3.07029648698129,-0.0021329558100943,
1.20842344717745));
#6696=CARTESIAN_POINT('Ctrl Pts',(-3.07262562444356,-0.359867988536013,
1.22690407211466));
#6697=CARTESIAN_POINT('Ctrl Pts',(-2.8500883529908,-1.73417835702742,1.29804575213475));
#6698=CARTESIAN_POINT('Ctrl Pts',(-0.82610974606013,-3.53132320122762,1.42184848723771));
#6699=CARTESIAN_POINT('Ctrl Pts',(2.50592737524966,-2.62168489533313,1.57983165248634));
#6700=CARTESIAN_POINT('Ctrl Pts',(3.56502744730094,0.665951678041991,1.73781481773498));
#6701=CARTESIAN_POINT('Ctrl Pts',(1.3905130838547,3.34952614641417,1.89579798298361));
#6702=CARTESIAN_POINT('Ctrl Pts',(-2.02101881154259,2.99747636377196,2.0526675261311));
#6703=CARTESIAN_POINT('Ctrl Pts',(-3.07658433315844,0.990670161723115,2.15687601419572));
#6704=CARTESIAN_POINT('Ctrl Pts',(-3.07837144959354,-0.000390310105173098,
2.20842344717746));
#6705=CARTESIAN_POINT('Origin',(0.,0.,-2.20842344717745));
#6706=CARTESIAN_POINT('',(-3.07033931526091,0.00363009148700105,0.208423447177454));
#6707=CARTESIAN_POINT('',(-3.0766916133949,-0.00189804245167501,0.291576552822545));
#6708=CARTESIAN_POINT('',(-3.0735,-1.43456032168185E-13,-2.20842344717745));
#6709=CARTESIAN_POINT('',(-0.793799282532864,2.9692229537457,0.));
#6710=CARTESIAN_POINT('Ctrl Pts',(-0.793799282532843,2.9692229537457,-1.11022302462516E-15));
#6711=CARTESIAN_POINT('Ctrl Pts',(-1.77625330176029,2.70657130793364,0.0526610550828771));
#6712=CARTESIAN_POINT('Ctrl Pts',(-2.87604924152809,1.66965640541239,0.122135537475362));
#6713=CARTESIAN_POINT('Ctrl Pts',(-3.07270725204059,0.328982361216722,0.191610019867847));
#6714=CARTESIAN_POINT('Ctrl Pts',(-3.07033931526091,0.00363009148700071,
0.208423447177454));
#6715=CARTESIAN_POINT('',(0.795570175323944,2.97434157986908,-1.73204294965629E-16));
#6716=CARTESIAN_POINT('Origin',(0.,0.,0.));
#6717=CARTESIAN_POINT('Ctrl Pts',(0.795572458610595,2.9743481795293,-4.90601483049691E-17));
#6718=CARTESIAN_POINT('Ctrl Pts',(-0.152115296302603,3.22551568492474,0.0509809153588237));
#6719=CARTESIAN_POINT('Ctrl Pts',(-2.21229639614352,2.76930588931089,0.148173099633005));
#6720=CARTESIAN_POINT('Ctrl Pts',(-3.06995895786669,0.887635565040844,0.245365283907187));
#6721=CARTESIAN_POINT('Ctrl Pts',(-3.0766916133949,-0.00189804245167461,
0.291576552822545));
#6722=CARTESIAN_POINT('Origin',(0.,0.,-2.20842344717745));
#6723=CARTESIAN_POINT('Ctrl Pts',(-3.0766916133949,-0.00189804245167473,
0.291576552822545));
#6724=CARTESIAN_POINT('Ctrl Pts',(-3.07763130168989,-0.126051775768505,
0.298026338990065));
#6725=CARTESIAN_POINT('Ctrl Pts',(-3.01464226329898,-1.26297686345005,0.357137180240463));
#6726=CARTESIAN_POINT('Ctrl Pts',(-1.59892885671069,-3.25553203106243,0.46890907657374));
#6727=CARTESIAN_POINT('Ctrl Pts',(1.85231282140687,-3.11779525816486,0.626892241822374));
#6728=CARTESIAN_POINT('Ctrl Pts',(3.62348061843826,-0.15274939435253,0.784875407071009));
#6729=CARTESIAN_POINT('Ctrl Pts',(2.10800845124216,2.95117859561544,0.942858572319642));
#6730=CARTESIAN_POINT('Ctrl Pts',(-1.31948921168312,3.3781127260263,1.10084173756828));
#6731=CARTESIAN_POINT('Ctrl Pts',(-2.96075827138585,1.43785809058675,1.21708106440258));
#6732=CARTESIAN_POINT('Ctrl Pts',(-3.07619044359204,0.213309857138166,1.280659336154));
#6733=CARTESIAN_POINT('Ctrl Pts',(-3.07427865213087,0.00268124138861233,
1.29157655282254));
#6734=CARTESIAN_POINT('Ctrl Pts',(-3.07033931526091,0.00363009148700071,
0.208423447177454));
#6735=CARTESIAN_POINT('Ctrl Pts',(-3.06529067677062,-0.690048053110911,
0.244271074950725));
#6736=CARTESIAN_POINT('Ctrl Pts',(-2.49208243053968,-2.41283008884042,0.332779757806875));
#6737=CARTESIAN_POINT('Ctrl Pts',(0.353891905593742,-3.60835904048448,0.473949495745902));
#6738=CARTESIAN_POINT('Ctrl Pts',(3.21549712367075,-1.67724424006994,0.631932660994537));
#6739=CARTESIAN_POINT('Ctrl Pts',(3.16174910309101,1.77718997587638,0.789915826243172));
#6740=CARTESIAN_POINT('Ctrl Pts',(0.239554143273228,3.61860888141612,0.947898991491804));
#6741=CARTESIAN_POINT('Ctrl Pts',(-2.53238151228791,2.3468476466272,1.08740153180324));
#6742=CARTESIAN_POINT('Ctrl Pts',(-3.06598868242385,0.659507943147289,1.17424301703178));
#6743=CARTESIAN_POINT('Ctrl Pts',(-3.07029648698129,-0.0021329558100943,
1.20842344717745));
#6744=CARTESIAN_POINT('Ctrl Pts',(1.91346599666506,-1.63598720337495,-2.77555756156289E-16));
#6745=CARTESIAN_POINT('Ctrl Pts',(2.45478008065218,-1.00286116724919,0.0526610550828779));
#6746=CARTESIAN_POINT('Ctrl Pts',(2.85088904111311,0.831797344758419,0.157983165248634));
#6747=CARTESIAN_POINT('Ctrl Pts',(0.857588690962395,2.84611954060091,0.315966330497269));
#6748=CARTESIAN_POINT('Ctrl Pts',(-1.91305892034906,2.27152017519409,0.473949495745902));
#6749=CARTESIAN_POINT('Ctrl Pts',(-2.94872155070904,-0.359723249961514,
0.631932660994538));
#6750=CARTESIAN_POINT('Ctrl Pts',(-1.30968062364378,-2.66660220862199,0.789915826243172));
#6751=CARTESIAN_POINT('Ctrl Pts',(1.51722711172663,-2.55378219047666,0.947898991491806));
#6752=CARTESIAN_POINT('Ctrl Pts',(2.96798843563309,-0.125116837573611,1.10588215674044));
#6753=CARTESIAN_POINT('Ctrl Pts',(1.72666708182923,2.41730669089373,1.26386532198907));
#6754=CARTESIAN_POINT('Ctrl Pts',(-1.08079196043997,2.76700790231697,1.42184848723771));
#6755=CARTESIAN_POINT('Ctrl Pts',(-2.90794013715773,0.607013050434708,1.57983165248634));
#6756=CARTESIAN_POINT('Ctrl Pts',(-2.09748509105245,-2.10360231788684,1.73781481773498));
#6757=CARTESIAN_POINT('Ctrl Pts',(0.615459340965577,-2.90615822119971,1.89579798298361));
#6758=CARTESIAN_POINT('Ctrl Pts',(2.77016176222782,-1.07274006639895,2.05378114823225));
#6759=CARTESIAN_POINT('Ctrl Pts',(2.41223259037106,1.7336955053395,2.21176431348088));
#6760=CARTESIAN_POINT('Ctrl Pts',(-0.133673706697308,2.96760717222605,2.36974747872952));
#6761=CARTESIAN_POINT('Ctrl Pts',(-2.55833347750605,1.50979936227371,2.52773064397815));
#6762=CARTESIAN_POINT('Ctrl Pts',(-2.66249741667059,-1.31744879591152,2.68571380922678));
#6763=CARTESIAN_POINT('Ctrl Pts',(-0.351685346285025,-2.94972551390458,
2.84369697447542));
#6764=CARTESIAN_POINT('Ctrl Pts',(2.27811734955878,-1.90650072719625,3.00168013972405));
#6765=CARTESIAN_POINT('Ctrl Pts',(2.84158984573739,0.865985405376183,3.15966330497269));
#6766=CARTESIAN_POINT('Ctrl Pts',(0.827643365721903,2.85299315809883,3.31764647022132));
#6767=CARTESIAN_POINT('Ctrl Pts',(-1.93700389804496,2.25223876861204,3.47562963546996));
#6768=CARTESIAN_POINT('Ctrl Pts',(-2.94472251124898,-0.391373073923526,
3.63361280071859));
#6769=CARTESIAN_POINT('Ctrl Pts',(-1.28147729755077,-2.67999617155092,3.79159596596722));
#6770=CARTESIAN_POINT('Ctrl Pts',(1.54411156485185,-2.53777127198967,3.94957913121586));
#6771=CARTESIAN_POINT('Ctrl Pts',(2.96913853395838,-0.0937012068447269,
4.10756229646449));
#6772=CARTESIAN_POINT('Ctrl Pts',(1.70105550977851,2.4353590499133,4.26554546171313));
#6773=CARTESIAN_POINT('Ctrl Pts',(-1.10994292249092,2.75546552502699,4.42352862696176));
#6774=CARTESIAN_POINT('Ctrl Pts',(-2.91418523928623,0.576270718626006,4.5815117922104));
#6775=CARTESIAN_POINT('Ctrl Pts',(-2.07516207671643,-2.12562129867421,4.73949495745903));
#6776=CARTESIAN_POINT('Ctrl Pts',(0.646103919259875,-2.89950224630314,4.89747812270767));
#6777=CARTESIAN_POINT('Ctrl Pts',(2.78133160738197,-1.04343568997828,5.0554612879563));
#6778=CARTESIAN_POINT('Ctrl Pts',(2.39379659512723,1.75906265128847,5.21344445320494));
#6779=CARTESIAN_POINT('Ctrl Pts',(-0.16499363494388,2.96603112830485,5.37142761845357));
#6780=CARTESIAN_POINT('Ctrl Pts',(-2.57412900533635,1.48270813296201,5.5294107837022));
#6781=CARTESIAN_POINT('Ctrl Pts',(-2.64844150963962,-1.34548174319338,5.68739394895084));
#6782=CARTESIAN_POINT('Ctrl Pts',(-0.320527163328734,-2.953273761345,5.84537711419947));
#6783=CARTESIAN_POINT('Ctrl Pts',(2.29811625201049,-1.8823456625252,6.00336027944811));
#6784=CARTESIAN_POINT('Ctrl Pts',(2.83228980319549,0.895934174165315,6.16134344469674));
#6785=CARTESIAN_POINT('Ctrl Pts',(0.797479800043391,2.8615711854999,6.31932660994538));
#6786=CARTESIAN_POINT('Ctrl Pts',(-1.9606715426706,2.23166536289225,6.47730977519401));
#6787=CARTESIAN_POINT('Ctrl Pts',(-2.94042698671483,-0.422436929523689,
6.63529294044265));
#6788=CARTESIAN_POINT('Ctrl Pts',(-1.25311457556089,-2.69337486380324,6.79327610569128));
#6789=CARTESIAN_POINT('Ctrl Pts',(1.57081511540494,-2.52132918551407,6.95125927093992));
#6790=CARTESIAN_POINT('Ctrl Pts',(2.96996266917328,-0.0623531795483424,
7.10924243618854));
#6791=CARTESIAN_POINT('Ctrl Pts',(1.67525120350748,2.45318177967176,7.26722560143719));
#6792=CARTESIAN_POINT('Ctrl Pts',(-1.13896739958789,2.74359236580518,7.42520876668581));
#6793=CARTESIAN_POINT('Ctrl Pts',(-2.92010921422275,0.545480151808999,7.58319193193445));
#6794=CARTESIAN_POINT('Ctrl Pts',(-2.0526017431469,-2.14741862912689,7.74117509718308));
#6795=CARTESIAN_POINT('Ctrl Pts',(0.67666536543526,-2.89250202704452,7.89915826243172));
#6796=CARTESIAN_POINT('Ctrl Pts',(2.79221254834523,-1.01405124829845,8.05714142768035));
#6797=CARTESIAN_POINT('Ctrl Pts',(2.37505367965917,1.78430087032248,8.21512459292899));
#6798=CARTESIAN_POINT('Ctrl Pts',(-0.196218413907403,2.96399728727909,8.37310775817763));
#6799=CARTESIAN_POINT('Ctrl Pts',(-2.58978452475258,1.45569460750793,8.53109092342626));
#6800=CARTESIAN_POINT('Ctrl Pts',(-2.63380935188005,-1.37382964669131,8.68907408867489));
#6801=CARTESIAN_POINT('Ctrl Pts',(-0.28987227158717,-2.95560017681787,8.84705725392352));
#6802=CARTESIAN_POINT('Ctrl Pts',(2.3189007506055,-1.85971882581699,9.00504041917216));
#6803=CARTESIAN_POINT('Ctrl Pts',(2.82058775165227,0.929376071735854,9.16302358442079));
#6804=CARTESIAN_POINT('Ctrl Pts',(1.45492685445962,2.21694916795929,9.26834569458655));
#6805=CARTESIAN_POINT('Ctrl Pts',(0.65019999797512,2.43208680203507,9.32100674966943));
#6806=CARTESIAN_POINT('Ctrl Pts',(2.05433155034209,-1.75642532122685,-0.107002249889811));
#6807=CARTESIAN_POINT('Ctrl Pts',(2.63549609850622,-1.07668980796293,-0.0543411948069327));
#6808=CARTESIAN_POINT('Ctrl Pts',(3.06076581130297,0.89303260774229,0.0509809153588233));
#6809=CARTESIAN_POINT('Ctrl Pts',(0.920722661458932,3.05564518966732,0.208964080607458));
#6810=CARTESIAN_POINT('Ctrl Pts',(-2.05389450587889,2.43874496399355,0.366947245856092));
#6811=CARTESIAN_POINT('Ctrl Pts',(-3.16580055530278,-0.386205358796813,
0.524930411104728));
#6812=CARTESIAN_POINT('Ctrl Pts',(-1.40609670133275,-2.86291214943547,0.682913576353361));
#6813=CARTESIAN_POINT('Ctrl Pts',(1.62892234828671,-2.74178654637273,0.840896741601996));
#6814=CARTESIAN_POINT('Ctrl Pts',(3.18648582990148,-0.13432768983325,0.99887990685063));
#6815=CARTESIAN_POINT('Ctrl Pts',(1.85378087163354,2.59526399246763,1.15686307209926));
#6816=CARTESIAN_POINT('Ctrl Pts',(-1.16035771085436,2.97070951022008,1.3148462373479));
#6817=CARTESIAN_POINT('Ctrl Pts',(-3.12201689535166,0.651700141602095,1.47282940259653));
#6818=CARTESIAN_POINT('Ctrl Pts',(-2.25189776376018,-2.25846532864422,1.63081256784517));
#6819=CARTESIAN_POINT('Ctrl Pts',(0.660768231210779,-3.12010379829167,1.7887957330938));
#6820=CARTESIAN_POINT('Ctrl Pts',(2.97409555101281,-1.15171305241918,1.94677889834243));
#6821=CARTESIAN_POINT('Ctrl Pts',(2.58981634677574,1.86132671367697,2.10476206359107));
#6822=CARTESIAN_POINT('Ctrl Pts',(-0.143514498610412,3.18607649864216,2.26274522883971));
#6823=CARTESIAN_POINT('Ctrl Pts',(-2.74667289008379,1.62094778272047,2.42072839408834));
#6824=CARTESIAN_POINT('Ctrl Pts',(-2.8585051708803,-1.41443675096306,2.57871155933698));
#6825=CARTESIAN_POINT('Ctrl Pts',(-0.377575720668934,-3.16687842826817,
2.7366947245856));
#6826=CARTESIAN_POINT('Ctrl Pts',(2.44582780918866,-2.0468535116148,2.89467788983425));
#6827=CARTESIAN_POINT('Ctrl Pts',(3.05078202769436,0.92973752525558,3.05266105508288));
#6828=CARTESIAN_POINT('Ctrl Pts',(0.888572821046812,3.06302482918826,3.21064422033151));
#6829=CARTESIAN_POINT('Ctrl Pts',(-2.07960226511719,2.41804409868132,3.36862738558015));
#6830=CARTESIAN_POINT('Ctrl Pts',(-3.16150711452663,-0.420185179729744,
3.52661055082878));
#6831=CARTESIAN_POINT('Ctrl Pts',(-1.37581710257403,-2.87729214922485,3.68459371607741));
#6832=CARTESIAN_POINT('Ctrl Pts',(1.65778598127789,-2.72459693597196,3.84257688132606));
#6833=CARTESIAN_POINT('Ctrl Pts',(3.18772059617366,-0.100599302972588,4.00056004657468));
#6834=CARTESIAN_POINT('Ctrl Pts',(1.82628382668507,2.61464533018498,4.15854321182332));
#6835=CARTESIAN_POINT('Ctrl Pts',(-1.19165470864185,2.95831740611471,4.31652637707195));
#6836=CARTESIAN_POINT('Ctrl Pts',(-3.12872174945414,0.618694620586424,4.47450954232059));
#6837=CARTESIAN_POINT('Ctrl Pts',(-2.22793137359221,-2.28210530291954,4.63249270756923));
#6838=CARTESIAN_POINT('Ctrl Pts',(0.693668802293106,-3.1129578237867,4.79047587281786));
#6839=CARTESIAN_POINT('Ctrl Pts',(2.98608769790887,-1.12025134620178,4.94845903806649));
#6840=CARTESIAN_POINT('Ctrl Pts',(2.57002313029978,1.88856133836114,5.10644220331513));
#6841=CARTESIAN_POINT('Ctrl Pts',(-0.177140137562721,3.18438442950809,5.26442536856376));
#6842=CARTESIAN_POINT('Ctrl Pts',(-2.76363125319693,1.59186215109202,5.42240853381239));
#6843=CARTESIAN_POINT('Ctrl Pts',(-2.84341449598317,-1.44453342796206,5.58039169906103));
#6844=CARTESIAN_POINT('Ctrl Pts',(-0.34412373437286,-3.1706878906145,5.73837486430966));
#6845=CARTESIAN_POINT('Ctrl Pts',(2.4672989909867,-2.0209201992169,5.89635802955829));
#6846=CARTESIAN_POINT('Ctrl Pts',(3.04079733455288,0.961891062723529,6.05434119480694));
#6847=CARTESIAN_POINT('Ctrl Pts',(0.856188673770513,3.07223435387301,6.21232436005557));
#6848=CARTESIAN_POINT('Ctrl Pts',(-2.10501227457723,2.39595611982943,6.3703075253042));
#6849=CARTESIAN_POINT('Ctrl Pts',(-3.15689536203605,-0.453535894477701,
6.52829069055284));
#6850=CARTESIAN_POINT('Ctrl Pts',(-1.34536637351016,-2.89165575414083,6.68627385580147));
#6851=CARTESIAN_POINT('Ctrl Pts',(1.68645539401005,-2.70694441585446,6.8442570210501));
#6852=CARTESIAN_POINT('Ctrl Pts',(3.18860540258081,-0.0669434963744089,
7.00224018629874));
#6853=CARTESIAN_POINT('Ctrl Pts',(1.79857985880707,2.63378013379257,7.16022335154736));
#6854=CARTESIAN_POINT('Ctrl Pts',(-1.22281590990512,2.94557016857085,7.31820651679601));
#6855=CARTESIAN_POINT('Ctrl Pts',(-3.13508183562068,0.585637313597254,7.47618968204465));
#6856=CARTESIAN_POINT('Ctrl Pts',(-2.20371019322167,-2.30550730940422,7.63417284729327));
#6857=CARTESIAN_POINT('Ctrl Pts',(0.726480121235595,-3.10544226233571,7.79215601254191));
#6858=CARTESIAN_POINT('Ctrl Pts',(2.9977696720632,-1.08870368048037,7.95013917779055));
#6859=CARTESIAN_POINT('Ctrl Pts',(2.54990039874432,1.9156575447878,8.10812234303918));
#6860=CARTESIAN_POINT('Ctrl Pts',(-0.210663622531375,3.18220086115888,8.26610550828781));
#6861=CARTESIAN_POINT('Ctrl Pts',(-2.78043930075555,1.56285994372434,8.42408867353645));
#6862=CARTESIAN_POINT('Ctrl Pts',(-2.8277051479271,-1.47496824762615,8.58207183878509));
#6863=CARTESIAN_POINT('Ctrl Pts',(-0.311212090587828,-3.17318557215857,
8.74005500403371));
#6864=CARTESIAN_POINT('Ctrl Pts',(2.48961360295064,-1.99662761987913,8.89803816928235));
#6865=CARTESIAN_POINT('Ctrl Pts',(3.02823380129393,0.997794886152954,9.05602133453098));
#6866=CARTESIAN_POINT('Ctrl Pts',(1.56203567022653,2.38015654795073,9.16134344469674));
#6867=CARTESIAN_POINT('Ctrl Pts',(0.69806642616104,2.61113218593861,9.21400449977962));
#6868=CARTESIAN_POINT('Ctrl Pts',(2.19519710401912,-1.87686343907875,-0.214004499779622));
#6869=CARTESIAN_POINT('Ctrl Pts',(2.81621211636026,-1.15051844867667,-0.161343444696743));
#6870=CARTESIAN_POINT('Ctrl Pts',(3.27064258149282,0.954267870726162,-0.0560213345309874));
#6871=CARTESIAN_POINT('Ctrl Pts',(0.983856631955468,3.26517083873374,0.101961830717648));
#6872=CARTESIAN_POINT('Ctrl Pts',(-2.19473009140873,2.60596975279301,0.259944995966281));
#6873=CARTESIAN_POINT('Ctrl Pts',(-3.38287955989652,-0.412687467632114,
0.417928161214917));
#6874=CARTESIAN_POINT('Ctrl Pts',(-1.50251277902172,-3.05922209024895,0.57591132646355));
#6875=CARTESIAN_POINT('Ctrl Pts',(1.74061758484679,-2.92979090226879,0.733894491712185));
#6876=CARTESIAN_POINT('Ctrl Pts',(3.40498322416987,-0.14353854209289,0.891877656960819));
#6877=CARTESIAN_POINT('Ctrl Pts',(1.98089466143785,2.77322129404153,1.04986082220945));
#6878=CARTESIAN_POINT('Ctrl Pts',(-1.23992346126874,3.17441111812319,1.20784398745809));
#6879=CARTESIAN_POINT('Ctrl Pts',(-3.3360936535456,0.696387232769482,1.36582715270672));
#6880=CARTESIAN_POINT('Ctrl Pts',(-2.40631043646792,-2.41332833940159,1.52381031795536));
#6881=CARTESIAN_POINT('Ctrl Pts',(0.706077121455976,-3.33404937538364,1.68179348320399));
#6882=CARTESIAN_POINT('Ctrl Pts',(3.1780293397978,-1.23068603843941,1.83977664845263));
#6883=CARTESIAN_POINT('Ctrl Pts',(2.76740010318042,1.98895792201444,1.99775981370126));
#6884=CARTESIAN_POINT('Ctrl Pts',(-0.153355290523512,3.40454582505827,2.1557429789499));
#6885=CARTESIAN_POINT('Ctrl Pts',(-2.93501230266153,1.73209620316724,2.31372614419853));
#6886=CARTESIAN_POINT('Ctrl Pts',(-3.05451292509001,-1.51142470601461,2.47170930944717));
#6887=CARTESIAN_POINT('Ctrl Pts',(-0.403466095052845,-3.38403134263174,
2.62969247469579));
#6888=CARTESIAN_POINT('Ctrl Pts',(2.61353826881855,-2.18720629603336,2.78767563994443));
#6889=CARTESIAN_POINT('Ctrl Pts',(3.25997420965132,0.993489645134981,2.94565880519306));
#6890=CARTESIAN_POINT('Ctrl Pts',(0.949502276371721,3.27305650027769,3.1036419704417));
#6891=CARTESIAN_POINT('Ctrl Pts',(-2.22220063218942,2.58384942875061,3.26162513569034));
#6892=CARTESIAN_POINT('Ctrl Pts',(-3.37829171780428,-0.448997285535967,
3.41960830093897));
#6893=CARTESIAN_POINT('Ctrl Pts',(-1.4701569075973,-3.07458812689877,3.5775914661876));
#6894=CARTESIAN_POINT('Ctrl Pts',(1.77146039770392,-2.91142259995426,3.73557463143624));
#6895=CARTESIAN_POINT('Ctrl Pts',(3.40630265838893,-0.107497399100449,3.89355779668488));
#6896=CARTESIAN_POINT('Ctrl Pts',(1.95151214359164,2.79393161045665,4.0515409619335));
#6897=CARTESIAN_POINT('Ctrl Pts',(-1.27336649479279,3.16116928720243,4.20952412718215));
#6898=CARTESIAN_POINT('Ctrl Pts',(-3.34325825962205,0.661118522546843,4.36750729243077));
#6899=CARTESIAN_POINT('Ctrl Pts',(-2.38070067046799,-2.43858930716488,4.52549045767941));
#6900=CARTESIAN_POINT('Ctrl Pts',(0.741233685326339,-3.32641340127025,4.68347362292804));
#6901=CARTESIAN_POINT('Ctrl Pts',(3.19084378843576,-1.19706700242527,4.84145678817668));
#6902=CARTESIAN_POINT('Ctrl Pts',(2.74624966547234,2.01806002543382,4.99943995342531));
#6903=CARTESIAN_POINT('Ctrl Pts',(-0.18928664018156,3.40273773071133,5.15742311867395));
#6904=CARTESIAN_POINT('Ctrl Pts',(-2.95313350105751,1.70101616922202,5.31540628392258));
#6905=CARTESIAN_POINT('Ctrl Pts',(-3.03838748232671,-1.54358511273075,5.47338944917122));
#6906=CARTESIAN_POINT('Ctrl Pts',(-0.36772030541699,-3.38810201988398,5.63137261441986));
#6907=CARTESIAN_POINT('Ctrl Pts',(2.63648172996291,-2.15949473590859,5.78935577966849));
#6908=CARTESIAN_POINT('Ctrl Pts',(3.24930486591027,1.02784795128174,5.94733894491712));
#6909=CARTESIAN_POINT('Ctrl Pts',(0.914897547497642,3.28289752224612,6.10532211016575));
#6910=CARTESIAN_POINT('Ctrl Pts',(-2.24935300648386,2.56024687676662,6.26330527541439));
#6911=CARTESIAN_POINT('Ctrl Pts',(-3.37336373735726,-0.484634859431713,
6.42128844066303));
#6912=CARTESIAN_POINT('Ctrl Pts',(-1.43761817145943,-3.08993664447841,6.57927160591165));
#6913=CARTESIAN_POINT('Ctrl Pts',(1.80209567261517,-2.89255964619486,6.7372547711603));
#6914=CARTESIAN_POINT('Ctrl Pts',(3.40724813598833,-0.071533813200476,6.89523793640892));
#6915=CARTESIAN_POINT('Ctrl Pts',(1.92190851410666,2.81437848791339,7.05322110165757));
#6916=CARTESIAN_POINT('Ctrl Pts',(-1.30666442022235,3.14754797133651,7.2112042669062));
#6917=CARTESIAN_POINT('Ctrl Pts',(-3.35005445701861,0.62579447538551,7.36918743215483));
#6918=CARTESIAN_POINT('Ctrl Pts',(-2.35481864329643,-2.46359598968156,7.52717059740347));
#6919=CARTESIAN_POINT('Ctrl Pts',(0.776294877035925,-3.31838249762691,7.6851537626521));
#6920=CARTESIAN_POINT('Ctrl Pts',(3.20332679578117,-1.16335611266229,7.84313692790073));
#6921=CARTESIAN_POINT('Ctrl Pts',(2.72474711782945,2.04701421925312,8.00112009314937));
#6922=CARTESIAN_POINT('Ctrl Pts',(-0.225108831155339,3.40040443503868,8.15910325839799));
#6923=CARTESIAN_POINT('Ctrl Pts',(-2.97109407675852,1.67002527994074,8.31708642364664));
#6924=CARTESIAN_POINT('Ctrl Pts',(-3.02160094397414,-1.57610684856099,8.47506958889527));
#6925=CARTESIAN_POINT('Ctrl Pts',(-0.332551909588488,-3.39077096749929,
8.63305275414391));
#6926=CARTESIAN_POINT('Ctrl Pts',(2.66032645529578,-2.13353641394126,8.79103591939254));
#6927=CARTESIAN_POINT('Ctrl Pts',(3.2358798509356,1.06621370057005,8.94901908464117));
#6928=CARTESIAN_POINT('Ctrl Pts',(1.66914448599343,2.54336392794217,9.05434119480693));
#6929=CARTESIAN_POINT('Ctrl Pts',(0.745932854346961,2.79017756984215,9.10700224988981));
#6930=CARTESIAN_POINT('Ctrl Pts',(2.33606265769615,-1.99730155693065,-0.321006749669432));
#6931=CARTESIAN_POINT('Ctrl Pts',(2.99692813421429,-1.22434708939042,-0.268345694586554));
#6932=CARTESIAN_POINT('Ctrl Pts',(3.48051935168267,1.01550313371003,-0.163023584420798));
#6933=CARTESIAN_POINT('Ctrl Pts',(1.04699060245201,3.47469648780015,-0.00504041917216321));
#6934=CARTESIAN_POINT('Ctrl Pts',(-2.33556567693856,2.77319454159246,0.152942746076471));
#6935=CARTESIAN_POINT('Ctrl Pts',(-3.59995856449026,-0.439169576467412,
0.310925911325106));
#6936=CARTESIAN_POINT('Ctrl Pts',(-1.59892885671069,-3.25553203106243,0.46890907657374));
#6937=CARTESIAN_POINT('Ctrl Pts',(1.85231282140687,-3.11779525816486,0.626892241822374));
#6938=CARTESIAN_POINT('Ctrl Pts',(3.62348061843826,-0.15274939435253,0.784875407071009));
#6939=CARTESIAN_POINT('Ctrl Pts',(2.10800845124216,2.95117859561544,0.942858572319642));
#6940=CARTESIAN_POINT('Ctrl Pts',(-1.31948921168312,3.3781127260263,1.10084173756828));
#6941=CARTESIAN_POINT('Ctrl Pts',(-3.55017041173953,0.741074323936872,1.25882490281691));
#6942=CARTESIAN_POINT('Ctrl Pts',(-2.56072310917565,-2.56819135015897,1.41680806806555));
#6943=CARTESIAN_POINT('Ctrl Pts',(0.751386011701174,-3.5479949524756,1.57479123331418));
#6944=CARTESIAN_POINT('Ctrl Pts',(3.3819631285828,-1.30965902445964,1.73277439856281));
#6945=CARTESIAN_POINT('Ctrl Pts',(2.94498385958509,2.11658913035191,1.89075756381145));
#6946=CARTESIAN_POINT('Ctrl Pts',(-0.163196082436613,3.62301515147438,2.04874072906008));
#6947=CARTESIAN_POINT('Ctrl Pts',(-3.12335171523926,1.843244623614,2.20672389430872));
#6948=CARTESIAN_POINT('Ctrl Pts',(-3.25052067929972,-1.60841266106616,2.36470705955735));
#6949=CARTESIAN_POINT('Ctrl Pts',(-0.429356469436753,-3.60118425699533,
2.52269022480598));
#6950=CARTESIAN_POINT('Ctrl Pts',(2.78124872844843,-2.32755908045191,2.68067339005463));
#6951=CARTESIAN_POINT('Ctrl Pts',(3.46916639160829,1.05724176501438,2.83865655530325));
#6952=CARTESIAN_POINT('Ctrl Pts',(1.01043173169663,3.48308817136713,2.99663972055189));
#6953=CARTESIAN_POINT('Ctrl Pts',(-2.36479899926165,2.74965475881989,3.15462288580052));
#6954=CARTESIAN_POINT('Ctrl Pts',(-3.59507632108192,-0.477809391342187,
3.31260605104916));
#6955=CARTESIAN_POINT('Ctrl Pts',(-1.56449671262057,-3.27188410457269,3.47058921629779));
#6956=CARTESIAN_POINT('Ctrl Pts',(1.88513481412996,-3.09824826393655,3.62857238154643));
#6957=CARTESIAN_POINT('Ctrl Pts',(3.6248847206042,-0.114395495228309,3.78655554679506));
#6958=CARTESIAN_POINT('Ctrl Pts',(2.07674046049821,2.97321789072832,3.9445387120437));
#6959=CARTESIAN_POINT('Ctrl Pts',(-1.35507828094373,3.36402116829015,4.10252187729233));
#6960=CARTESIAN_POINT('Ctrl Pts',(-3.55779476978996,0.703542424507262,4.26050504254097));
#6961=CARTESIAN_POINT('Ctrl Pts',(-2.53346996734378,-2.59507331141021,4.4184882077896));
#6962=CARTESIAN_POINT('Ctrl Pts',(0.788798568359572,-3.5398689787538,4.57647137303824));
#6963=CARTESIAN_POINT('Ctrl Pts',(3.39559987896266,-1.27388265864876,4.73445453828687));
#6964=CARTESIAN_POINT('Ctrl Pts',(2.92247620064489,2.14755871250649,4.8924377035355));
#6965=CARTESIAN_POINT('Ctrl Pts',(-0.201433142800403,3.62109103191458,5.05042086878414));
#6966=CARTESIAN_POINT('Ctrl Pts',(-3.14263574891808,1.81017018735203,5.20840403403277));
#6967=CARTESIAN_POINT('Ctrl Pts',(-3.23336046867026,-1.64263679749944,5.36638719928141));
#6968=CARTESIAN_POINT('Ctrl Pts',(-0.391316876461119,-3.60551614915347,
5.52437036453005));
#6969=CARTESIAN_POINT('Ctrl Pts',(2.80566446893912,-2.29806927260028,5.68235352977867));
#6970=CARTESIAN_POINT('Ctrl Pts',(3.45781239726766,1.09380483983996,5.84033669502732));
#6971=CARTESIAN_POINT('Ctrl Pts',(0.97360642122477,3.49356069061924,5.99831986027594));
#6972=CARTESIAN_POINT('Ctrl Pts',(-2.3936937383905,2.7245376337038,6.15630302552459));
#6973=CARTESIAN_POINT('Ctrl Pts',(-3.58983211267847,-0.515733824385723,
6.31428619077321));
#6974=CARTESIAN_POINT('Ctrl Pts',(-1.5298699694087,-3.288217534816,6.47226935602186));
#6975=CARTESIAN_POINT('Ctrl Pts',(1.91773595122029,-3.07817487653525,6.63025252127048));
#6976=CARTESIAN_POINT('Ctrl Pts',(3.62589086939586,-0.0761241300265441,
6.78823568651912));
#6977=CARTESIAN_POINT('Ctrl Pts',(2.04523716940625,2.99497684203422,6.94621885176775));
#6978=CARTESIAN_POINT('Ctrl Pts',(-1.39051293053958,3.34952577410217,7.10420201701639));
#6979=CARTESIAN_POINT('Ctrl Pts',(-3.56502707841653,0.665951637173768,7.26218518226502));
#6980=CARTESIAN_POINT('Ctrl Pts',(-2.5059270933712,-2.62168466995889,7.42016834751365));
#6981=CARTESIAN_POINT('Ctrl Pts',(0.826109632836259,-3.5313227329181,7.57815151276229));
#6982=CARTESIAN_POINT('Ctrl Pts',(3.40888391949913,-1.23800854484421,7.73613467801092));
#6983=CARTESIAN_POINT('Ctrl Pts',(2.89959383691459,2.17837089371843,7.89411784325955));
#6984=CARTESIAN_POINT('Ctrl Pts',(-0.239554039779309,3.61860800891848,8.0521010085082));
#6985=CARTESIAN_POINT('Ctrl Pts',(-3.16174885276149,1.77719061615714,8.21008417375682));
#6986=CARTESIAN_POINT('Ctrl Pts',(-3.21549674002119,-1.67724544949582,8.36806733900547));
#6987=CARTESIAN_POINT('Ctrl Pts',(-0.353891728589143,-3.60835636284,8.52605050425409));
#6988=CARTESIAN_POINT('Ctrl Pts',(2.83103930764092,-2.27044520800339,8.68403366950274));
#6989=CARTESIAN_POINT('Ctrl Pts',(3.44352590057726,1.13463251498715,8.84201683475136));
#6990=CARTESIAN_POINT('Ctrl Pts',(1.77625330176034,2.70657130793361,8.94733894491712));
#6991=CARTESIAN_POINT('Ctrl Pts',(0.793799282532882,2.96922295374569,9.));
#6992=CARTESIAN_POINT('Ctrl Pts',(0.793799282532882,2.96922295374569,9.));
#6993=CARTESIAN_POINT('Ctrl Pts',(0.886878490836273,2.9351741635662,9.));
#6994=CARTESIAN_POINT('Ctrl Pts',(0.977892261281868,2.89636065937617,9.));
#6995=CARTESIAN_POINT('Ctrl Pts',(1.0666317018473,2.85310967040871,9.));
#6996=CARTESIAN_POINT('Ctrl Pts',(1.15732414289755,2.80890680252603,9.));
#6997=CARTESIAN_POINT('Ctrl Pts',(1.24564171258029,2.76006836197957,9.));
#6998=CARTESIAN_POINT('Ctrl Pts',(1.33133249020885,2.70689814911949,9.));
#6999=CARTESIAN_POINT('Ctrl Pts',(1.41378164632743,2.65573932780546,9.));
#7000=CARTESIAN_POINT('Ctrl Pts',(1.49379927546973,2.60056939696339,9.));
#7001=CARTESIAN_POINT('Ctrl Pts',(1.57112798504849,2.54162891700393,9.));
#7002=CARTESIAN_POINT('Ctrl Pts',(1.6387906059299,2.4900559970394,9.));
#7003=CARTESIAN_POINT('Ctrl Pts',(1.70439423245071,2.43559555361028,9.));
#7004=CARTESIAN_POINT('Ctrl Pts',(1.76774178614759,2.37839602731573,9.));
#7005=CARTESIAN_POINT('Ctrl Pts',(1.78181925285965,2.36568481148552,9.));
#7006=CARTESIAN_POINT('Ctrl Pts',(1.79578788660031,2.35283565182172,8.99999999999999));
#7007=CARTESIAN_POINT('Ctrl Pts',(1.80962611638746,2.33986853565167,8.99999999999999));
#7008=CARTESIAN_POINT('Ctrl Pts',(1.88206130473834,2.27199312697639,8.99999999999999));
#7009=CARTESIAN_POINT('Ctrl Pts',(1.95103093355494,2.20079709720709,9.));
#7010=CARTESIAN_POINT('Ctrl Pts',(2.01629483992911,2.12656978280043,9.));
#7011=CARTESIAN_POINT('Ctrl Pts',(2.0811938619788,2.05275746628435,9.));
#7012=CARTESIAN_POINT('Ctrl Pts',(2.14242896847189,1.97594687106671,9.));
#7013=CARTESIAN_POINT('Ctrl Pts',(2.19972040363224,1.89639573891051,9.));
#7014=CARTESIAN_POINT('Ctrl Pts',(2.25491851002233,1.81975126589425,9.));
#7015=CARTESIAN_POINT('Ctrl Pts',(2.30645603825338,1.74056213090656,9.));
#7016=CARTESIAN_POINT('Ctrl Pts',(2.35403785390585,1.65904519358341,9.));
#7017=CARTESIAN_POINT('Ctrl Pts',(2.37402534994049,1.62480271167807,9.));
#7018=CARTESIAN_POINT('Ctrl Pts',(2.3933142673739,1.59014936887301,9.));
#7019=CARTESIAN_POINT('Ctrl Pts',(2.41188012691626,1.55510093684168,9.));
#7020=CARTESIAN_POINT('Ctrl Pts',(2.42490948045064,1.53050426192231,9.));
#7021=CARTESIAN_POINT('Ctrl Pts',(2.43758268759006,1.50571299850418,8.99999999999999));
#7022=CARTESIAN_POINT('Ctrl Pts',(2.44989080186182,1.48073259132809,8.99999999999999));
#7023=CARTESIAN_POINT('Ctrl Pts',(2.45765276114193,1.46497900803983,8.99999999999999));
#7024=CARTESIAN_POINT('Ctrl Pts',(2.46527041180683,1.44914804972639,9.));
#7025=CARTESIAN_POINT('Ctrl Pts',(2.47273181388943,1.43326226638681,9.));
#7026=CARTESIAN_POINT('Ctrl Pts',(2.51485724445469,1.34357463722026,9.));
#7027=CARTESIAN_POINT('Ctrl Pts',(2.55207933717843,1.25199813943898,8.99999999999999));
#7028=CARTESIAN_POINT('Ctrl Pts',(2.58410618468256,1.15880393051645,8.99999999999999));
#7029=CARTESIAN_POINT('Ctrl Pts',(2.613967295916,1.07191174924295,8.99999999999999));
#7030=CARTESIAN_POINT('Ctrl Pts',(2.63931185864415,0.983612456000679,8.99999999999999));
#7031=CARTESIAN_POINT('Ctrl Pts',(2.65985272591902,0.894117096452653,8.99999999999999));
#7032=CARTESIAN_POINT('Ctrl Pts',(2.66134249302584,0.88762626814031,8.99999999999999));
#7033=CARTESIAN_POINT('Ctrl Pts',(2.66280696907164,0.881129147123167,9.));
#7034=CARTESIAN_POINT('Ctrl Pts',(2.66424603364624,0.874625813581576,9.));
#7035=CARTESIAN_POINT('Ctrl Pts',(2.68483036310423,0.781602357540593,9.));
#7036=CARTESIAN_POINT('Ctrl Pts',(2.70021964474849,0.687306813520904,8.99999999999999));
#7037=CARTESIAN_POINT('Ctrl Pts',(2.71049110049637,0.592148341441679,8.99999999999999));
#7038=CARTESIAN_POINT('Ctrl Pts',(2.71630602466642,0.538276785854983,8.99999999999999));
#7039=CARTESIAN_POINT('Ctrl Pts',(2.72047976538942,0.484128852777968,8.99999999999999));
#7040=CARTESIAN_POINT('Ctrl Pts',(2.72301944391314,0.429781474340432,8.99999999999999));
#7041=CARTESIAN_POINT('Ctrl Pts',(2.72366615629779,0.415942272890204,8.99999999999999));
#7042=CARTESIAN_POINT('Ctrl Pts',(2.72420675980841,0.402091536187543,8.99999999999999));
#7043=CARTESIAN_POINT('Ctrl Pts',(2.72464119129261,0.388242780953578,8.99999999999999));
#7044=CARTESIAN_POINT('Ctrl Pts',(2.72756592883874,0.295008344975862,8.99999999999999));
#7045=CARTESIAN_POINT('Ctrl Pts',(2.72569048952638,0.201712560084688,8.99999999999999));
#7046=CARTESIAN_POINT('Ctrl Pts',(2.71914995708096,0.108731817539428,8.99999999999999));
#7047=CARTESIAN_POINT('Ctrl Pts',(2.71259904187879,0.0156034728777771,8.99999999999999));
#7048=CARTESIAN_POINT('Ctrl Pts',(2.70136783128446,-0.0772098102983187,
9.));
#7049=CARTESIAN_POINT('Ctrl Pts',(2.68554114262277,-0.169317716284785,9.));
#7050=CARTESIAN_POINT('Ctrl Pts',(2.66994282533527,-0.26009655025162,9.));
#7051=CARTESIAN_POINT('Ctrl Pts',(2.64988023184904,-0.350191061744686,8.99999999999999));
#7052=CARTESIAN_POINT('Ctrl Pts',(2.62539158794444,-0.439202338063852,8.99999999999999));
#7053=CARTESIAN_POINT('Ctrl Pts',(2.61615142083263,-0.472788479919204,8.99999999999999));
#7054=CARTESIAN_POINT('Ctrl Pts',(2.60628069313125,-0.506220073097839,8.99999999999999));
#7055=CARTESIAN_POINT('Ctrl Pts',(2.59578003712001,-0.539474360311661,8.99999999999999));
#7056=CARTESIAN_POINT('Ctrl Pts',(2.58810284762471,-0.563787076031328,8.99999999999999));
#7057=CARTESIAN_POINT('Ctrl Pts',(2.58008892698161,-0.588005000779692,9.));
#7058=CARTESIAN_POINT('Ctrl Pts',(2.57173827761392,-0.612118947017522,9.));
#7059=CARTESIAN_POINT('Ctrl Pts',(2.56654744841136,-0.627108365302125,9.));
#7060=CARTESIAN_POINT('Ctrl Pts',(2.56122944831744,-0.642049055238963,9.));
#7061=CARTESIAN_POINT('Ctrl Pts',(2.55578559038208,-0.656936550189778,9.));
#7062=CARTESIAN_POINT('Ctrl Pts',(2.52407277337967,-0.74366261993773,9.));
#7063=CARTESIAN_POINT('Ctrl Pts',(2.48808278639107,-0.828614124972656,8.99999999999999));
#7064=CARTESIAN_POINT('Ctrl Pts',(2.44787615884381,-0.911389078637309,8.99999999999999));
#7065=CARTESIAN_POINT('Ctrl Pts',(2.41772118818337,-0.973470293885799,8.99999999999999));
#7066=CARTESIAN_POINT('Ctrl Pts',(2.38519336783533,-1.03432671407457,9.));
#7067=CARTESIAN_POINT('Ctrl Pts',(2.35030314291149,-1.09377373790908,9.));
#7068=CARTESIAN_POINT('Ctrl Pts',(2.33453824589156,-1.12063444777661,9.));
#7069=CARTESIAN_POINT('Ctrl Pts',(2.31829087129828,-1.14720721377719,8.99999999999999));
#7070=CARTESIAN_POINT('Ctrl Pts',(2.30156120509674,-1.17347393974025,8.99999999999999));
#7071=CARTESIAN_POINT('Ctrl Pts',(2.2924219311199,-1.18782322813365,8.99999999999999));
#7072=CARTESIAN_POINT('Ctrl Pts',(2.28314386923737,-1.2020730730672,8.99999999999999));
#7073=CARTESIAN_POINT('Ctrl Pts',(2.27372778298295,-1.21622031438468,8.99999999999999));
#7074=CARTESIAN_POINT('Ctrl Pts',(2.22615751395616,-1.2876924799188,9.));
#7075=CARTESIAN_POINT('Ctrl Pts',(2.1750638810293,-1.35655384480895,9.));
#7076=CARTESIAN_POINT('Ctrl Pts',(2.12047811064926,-1.42245018095699,9.));
#7077=CARTESIAN_POINT('Ctrl Pts',(2.07432912024645,-1.47816157539741,9.));
#7078=CARTESIAN_POINT('Ctrl Pts',(2.02568338366803,-1.53175330505423,9.));
#7079=CARTESIAN_POINT('Ctrl Pts',(1.9745434647085,-1.58298712738403,9.));
#7080=CARTESIAN_POINT('Ctrl Pts',(1.95571094048283,-1.60185423198313,9.));
#7081=CARTESIAN_POINT('Ctrl Pts',(1.93654003149783,-1.62040132784491,9.));
#7082=CARTESIAN_POINT('Ctrl Pts',(1.91704088636911,-1.63862413454171,9.));
#7083=CARTESIAN_POINT('Ctrl Pts',(1.91346599666506,-1.63598720337495,-2.77555756156289E-16));
#7084=CARTESIAN_POINT('Ctrl Pts',(1.97510134314003,-1.57806511239367,-2.79433823621938E-16));
#7085=CARTESIAN_POINT('Ctrl Pts',(2.03336881374227,-1.51699406877496,-6.96361421210227E-16));
#7086=CARTESIAN_POINT('Ctrl Pts',(2.08826993179399,-1.45315846421965,-6.07153216591882E-16));
#7087=CARTESIAN_POINT('Ctrl Pts',(2.14462172708504,-1.38763610242017,-5.15587822965493E-16));
#7088=CARTESIAN_POINT('Ctrl Pts',(2.19742735662698,-1.31920071895718,-2.3862995218317E-16));
#7089=CARTESIAN_POINT('Ctrl Pts',(2.24666298209029,-1.24821943486301,-1.59594559789866E-16));
#7090=CARTESIAN_POINT('Ctrl Pts',(2.29723880045605,-1.1753060414018,-7.84078253361845E-17));
#7091=CARTESIAN_POINT('Ctrl Pts',(2.34404815214704,-1.09970570501749,-1.73347562424884E-16));
#7092=CARTESIAN_POINT('Ctrl Pts',(2.38703114656335,-1.02177339518613,-6.93889390390723E-17));
#7093=CARTESIAN_POINT('Ctrl Pts',(2.40590762936263,-0.98754851332257,-2.37342983415729E-17));
#7094=CARTESIAN_POINT('Ctrl Pts',(2.42404566668818,-0.95287338422101,-3.73213098570097E-17));
#7095=CARTESIAN_POINT('Ctrl Pts',(2.44143777842235,-0.917776011982524,-2.77555756156289E-17));
#7096=CARTESIAN_POINT('Ctrl Pts',(2.45136231257179,-0.897748250278805,-2.22970402983493E-17));
#7097=CARTESIAN_POINT('Ctrl Pts',(2.46104392774577,-0.87758297572818,-3.33298356902162E-16));
#7098=CARTESIAN_POINT('Ctrl Pts',(2.47048100099708,-0.857285244332943,-3.46944695195361E-16));
#7099=CARTESIAN_POINT('Ctrl Pts',(2.47900168762219,-0.838958523344988,-3.59265906346346E-16));
#7100=CARTESIAN_POINT('Ctrl Pts',(2.48732540306445,-0.820518075787568,-6.44662433235081E-16));
#7101=CARTESIAN_POINT('Ctrl Pts',(2.49543725255318,-0.801999440640286,-6.24500451351651E-16));
#7102=CARTESIAN_POINT('Ctrl Pts',(2.53203160380214,-0.71845777234719,-5.33545281640661E-16));
#7103=CARTESIAN_POINT('Ctrl Pts',(2.56436439720616,-0.633232805885642,-1.7353518107917E-16));
#7104=CARTESIAN_POINT('Ctrl Pts',(2.59240963609592,-0.546722656501286,-2.22044604925031E-16));
#7105=CARTESIAN_POINT('Ctrl Pts',(2.62091418406923,-0.458795692748289,-2.71348488718176E-16));
#7106=CARTESIAN_POINT('Ctrl Pts',(2.64499008370221,-0.369540350457117,-6.24020080701783E-16));
#7107=CARTESIAN_POINT('Ctrl Pts',(2.66457097387791,-0.279337521515105,-6.66133814775094E-16));
#7108=CARTESIAN_POINT('Ctrl Pts',(2.68356661536034,-0.191830744044346,-7.06988821200503E-16));
#7109=CARTESIAN_POINT('Ctrl Pts',(2.69833209310255,-0.103431355980504,-8.41126525273291E-16));
#7110=CARTESIAN_POINT('Ctrl Pts',(2.70876601617631,-0.0144652215165946,
-9.29811783123569E-16));
#7111=CARTESIAN_POINT('Ctrl Pts',(2.71312946546923,0.0227402680942152,-9.66899810601249E-16));
#7112=CARTESIAN_POINT('Ctrl Pts',(2.71673485533152,0.0600450673053063,-4.75178540744584E-16));
#7113=CARTESIAN_POINT('Ctrl Pts',(2.71957245241254,0.0974259566605276,-4.71844785465692E-16));
#7114=CARTESIAN_POINT('Ctrl Pts',(2.72134694520476,0.120802115020483,-4.69760019889566E-16));
#7115=CARTESIAN_POINT('Ctrl Pts',(2.7228211544872,0.144208034837555,-4.55034229124723E-16));
#7116=CARTESIAN_POINT('Ctrl Pts',(2.7239924097264,0.167638070156344,-4.44089209850063E-16));
#7117=CARTESIAN_POINT('Ctrl Pts',(2.72467909724156,0.181374711150338,-4.37672326631462E-16));
#7118=CARTESIAN_POINT('Ctrl Pts',(2.72526137600902,0.195115066492318,-8.40764763959006E-16));
#7119=CARTESIAN_POINT('Ctrl Pts',(2.72573871993999,0.208849770915952,-8.32667268468867E-16));
#7120=CARTESIAN_POINT('Ctrl Pts',(2.72911188874676,0.305906575299357,-7.75446012623746E-16));
#7121=CARTESIAN_POINT('Ctrl Pts',(2.7272553636767,0.402801526105327,-9.68836665814074E-16));
#7122=CARTESIAN_POINT('Ctrl Pts',(2.72010339077746,0.499113381476287,-9.15933995315754E-16));
#7123=CARTESIAN_POINT('Ctrl Pts',(2.71295141787821,0.595425236847248,-8.63031324817435E-16));
#7124=CARTESIAN_POINT('Ctrl Pts',(2.70050443398604,0.691155049107752,-7.97669397634917E-16));
#7125=CARTESIAN_POINT('Ctrl Pts',(2.68264379028147,0.785900518836936,-7.7715611723761E-16));
#7126=CARTESIAN_POINT('Ctrl Pts',(2.66557036541062,0.876470023835268,-7.30823456910502E-16));
#7127=CARTESIAN_POINT('Ctrl Pts',(2.64355009898795,0.966141014464811,-6.44790703633136E-16));
#7128=CARTESIAN_POINT('Ctrl Pts',(2.61685826648582,1.0546735630477,-5.82867087928207E-16));
#7129=CARTESIAN_POINT('Ctrl Pts',(2.60792689184721,1.08429750734011,-5.62146779167304E-16));
#7130=CARTESIAN_POINT('Ctrl Pts',(2.59847203287526,1.11379395063906,-3.30994876511457E-16));
#7131=CARTESIAN_POINT('Ctrl Pts',(2.58850272866474,1.14315372665541,-3.33066907387547E-16));
#7132=CARTESIAN_POINT('Ctrl Pts',(2.58205412116549,1.16214498901409,-3.34407192884316E-16));
#7133=CARTESIAN_POINT('Ctrl Pts',(2.57539025197676,1.18107906596373,-3.83440297547856E-16));
#7134=CARTESIAN_POINT('Ctrl Pts',(2.56851343345694,1.1999534423939,-3.88578058618805E-16));
#7135=CARTESIAN_POINT('Ctrl Pts',(2.56187577896064,1.21817140019159,-3.93537137119301E-16));
#7136=CARTESIAN_POINT('Ctrl Pts',(2.5550379237584,1.23633808433789,-5.11405226480168E-17));
#7137=CARTESIAN_POINT('Ctrl Pts',(2.54801290532315,1.2544236637051,-8.32667268468867E-17));
#7138=CARTESIAN_POINT('Ctrl Pts',(2.51416596007442,1.34156103142528,-2.38052637316906E-16));
#7139=CARTESIAN_POINT('Ctrl Pts',(2.47593990461506,1.42692801454723,-3.20308050061359E-16));
#7140=CARTESIAN_POINT('Ctrl Pts',(2.43366643270999,1.51029042462874,-3.60822483003176E-16));
#7141=CARTESIAN_POINT('Ctrl Pts',(2.38981735466084,1.59675989735712,-4.02846959634101E-16));
#7142=CARTESIAN_POINT('Ctrl Pts',(2.34161340681444,1.68107330940561,-3.78619360334886E-16));
#7143=CARTESIAN_POINT('Ctrl Pts',(2.28936877468746,1.76296634463835,-4.16333634234434E-16));
#7144=CARTESIAN_POINT('Ctrl Pts',(2.23653118032041,1.84578884335166,-4.54475954794925E-16));
#7145=CARTESIAN_POINT('Ctrl Pts',(2.17956025026491,1.92613653330701,-4.81277067279742E-16));
#7146=CARTESIAN_POINT('Ctrl Pts',(2.11872917895946,2.00372118802566,-3.33066907387547E-16));
#7147=CARTESIAN_POINT('Ctrl Pts',(2.07707986191238,2.05684121062297,-2.31591595405106E-16));
#7148=CARTESIAN_POINT('Ctrl Pts',(2.03361992333023,2.10866568467281,-4.99150862322262E-16));
#7149=CARTESIAN_POINT('Ctrl Pts',(1.98842485791504,2.15909508034387,-5.55111512312578E-16));
#7150=CARTESIAN_POINT('Ctrl Pts',(1.97697062272433,2.17187590394121,-5.69294176736786E-16));
#7151=CARTESIAN_POINT('Ctrl Pts',(1.96540341059899,2.18456858588751,-5.43387176388567E-16));
#7152=CARTESIAN_POINT('Ctrl Pts',(1.95373682360776,2.19715826975418,-5.55111512312578E-16));
#7153=CARTESIAN_POINT('Ctrl Pts',(1.88513632513593,2.27118665436278,-6.24051579295601E-16));
#7154=CARTESIAN_POINT('Ctrl Pts',(1.81301954111561,2.34175145938146,-9.96121943412486E-16));
#7155=CARTESIAN_POINT('Ctrl Pts',(1.7376981084074,2.40856242043656,-8.32667268468867E-16));
#7156=CARTESIAN_POINT('Ctrl Pts',(1.67462785275174,2.4645064491524,-6.95798813287656E-16));
#7157=CARTESIAN_POINT('Ctrl Pts',(1.60930957241425,2.51781846345041,-7.13394759801054E-17));
#7158=CARTESIAN_POINT('Ctrl Pts',(1.54190225473945,2.56831419612331,-5.55111512312578E-17));
#7159=CARTESIAN_POINT('Ctrl Pts',(1.50803147786761,2.59368725283794,-4.75577468485228E-17));
#7160=CARTESIAN_POINT('Ctrl Pts',(1.47363293052346,2.61834900472236,-3.20435029838497E-16));
#7161=CARTESIAN_POINT('Ctrl Pts',(1.43872500006545,2.64227442481775,-3.33066907387547E-16));
#7162=CARTESIAN_POINT('Ctrl Pts',(1.42333727249881,2.6528209637135,-3.38635151847466E-16));
#7163=CARTESIAN_POINT('Ctrl Pts',(1.40785826547886,2.66321910753516,-4.40548340244713E-16));
#7164=CARTESIAN_POINT('Ctrl Pts',(1.3922911852266,2.67346618319487,-3.88578058618805E-16));
#7165=CARTESIAN_POINT('Ctrl Pts',(1.30709626507894,2.72954598611418,-1.04157093259739E-16));
#7166=CARTESIAN_POINT('Ctrl Pts',(1.21925397020065,2.78111238575669,5.889711510458E-17));
#7167=CARTESIAN_POINT('Ctrl Pts',(1.12905315937313,2.8278552735782,5.55111512312578E-17));
#7168=CARTESIAN_POINT('Ctrl Pts',(1.04989346616971,2.86887655293752,5.25396495457291E-17));
#7169=CARTESIAN_POINT('Ctrl Pts',(0.968916412162158,2.90618287529182,-1.56714687611455E-16));
#7170=CARTESIAN_POINT('Ctrl Pts',(0.886294660306285,2.939540402264,-2.77555756156289E-16));
#7171=CARTESIAN_POINT('Ctrl Pts',(0.856267218376713,2.95166361656982,-3.21473345494835E-16));
#7172=CARTESIAN_POINT('Ctrl Pts',(0.826022362315256,2.96326500943248,-4.61516649787808E-17));
#7173=CARTESIAN_POINT('Ctrl Pts',(0.795572458610595,2.9743481795293,-5.55111512312578E-17));
#7174=CARTESIAN_POINT('Ctrl Pts',(-2.51342302570288,-0.000307789261743824,
8.61258330249198));
#7175=CARTESIAN_POINT('Ctrl Pts',(-2.51312706795389,0.431039503037857,8.58541917613674));
#7176=CARTESIAN_POINT('Ctrl Pts',(-2.40775786821181,0.862561153211593,8.5582550497815));
#7177=CARTESIAN_POINT('Ctrl Pts',(-2.19819431079963,1.23549101176992,8.53109092342626));
#7178=CARTESIAN_POINT('Ctrl Pts',(-1.79192915447086,1.95846216743165,8.47842986834338));
#7179=CARTESIAN_POINT('Ctrl Pts',(-0.994073784189135,2.46122972735536,8.42576881326051));
#7180=CARTESIAN_POINT('Ctrl Pts',(-0.166600750120509,2.51599743782446,8.37310775817763));
#7181=CARTESIAN_POINT('Ctrl Pts',(0.660872283948123,2.57076514829355,8.32044670309475));
#7182=CARTESIAN_POINT('Ctrl Pts',(1.51796298180366,2.17753300930801,8.26778564801187));
#7183=CARTESIAN_POINT('Ctrl Pts',(2.01603480884577,1.51452492004508,8.21512459292899));
#7184=CARTESIAN_POINT('Ctrl Pts',(2.51410663588786,0.85151683078216,8.16246353784611));
#7185=CARTESIAN_POINT('Ctrl Pts',(2.65315959211654,-0.0812672087581283,
8.10980248276323));
#7186=CARTESIAN_POINT('Ctrl Pts',(2.37009487307924,-0.860734358319284,8.05714142768036));
#7187=CARTESIAN_POINT('Ctrl Pts',(2.08703015404192,-1.64020150788046,8.00448037259748));
#7188=CARTESIAN_POINT('Ctrl Pts',(1.38184775973859,-2.26635176746249,7.9518193175146));
#7189=CARTESIAN_POINT('Ctrl Pts',(0.574378711156563,-2.4552463309339,7.89915826243172));
#7190=CARTESIAN_POINT('Ctrl Pts',(-0.233090337425462,-2.64414089440531,
7.84649720734884));
#7191=CARTESIAN_POINT('Ctrl Pts',(-1.1428460402862,-2.39577976176609,7.79383615226596));
#7192=CARTESIAN_POINT('Ctrl Pts',(-1.7423084702292,-1.82278273195717,7.74117509718308));
#7193=CARTESIAN_POINT('Ctrl Pts',(-2.23024621723499,-1.35638673147292,7.69831116561938));
#7194=CARTESIAN_POINT('Ctrl Pts',(-2.51260567208493,-0.674910034313931,
7.65544723405568));
#7195=CARTESIAN_POINT('Ctrl Pts',(-2.5186623288877,0.00210982157644382,
7.61258330249198));
#7196=CARTESIAN_POINT('Ctrl Pts',(-0.793799282532843,2.9692229537457,-1.11022302462516E-15));
#7197=CARTESIAN_POINT('Ctrl Pts',(-1.77625330176029,2.70657130793364,0.0526610550828771));
#7198=CARTESIAN_POINT('Ctrl Pts',(-3.44352486880409,1.13462630258776,0.157983165248634));
#7199=CARTESIAN_POINT('Ctrl Pts',(-2.83104022223192,-2.27044164625735,0.315966330497268));
#7200=CARTESIAN_POINT('Ctrl Pts',(0.353891905593742,-3.60835904048448,0.473949495745902));
#7201=CARTESIAN_POINT('Ctrl Pts',(3.21549712367075,-1.67724424006994,0.631932660994537));
#7202=CARTESIAN_POINT('Ctrl Pts',(3.16174910309101,1.77718997587638,0.789915826243172));
#7203=CARTESIAN_POINT('Ctrl Pts',(0.239554143273228,3.61860888141612,0.947898991491804));
#7204=CARTESIAN_POINT('Ctrl Pts',(-2.8995942030829,2.17837084084757,1.10588215674044));
#7205=CARTESIAN_POINT('Ctrl Pts',(-3.40888424173261,-1.23800851265563,1.26386532198907));
#7206=CARTESIAN_POINT('Ctrl Pts',(-0.82610974606013,-3.53132320122762,1.42184848723771));
#7207=CARTESIAN_POINT('Ctrl Pts',(2.50592737524966,-2.62168489533313,1.57983165248634));
#7208=CARTESIAN_POINT('Ctrl Pts',(3.56502744730094,0.665951678041991,1.73781481773498));
#7209=CARTESIAN_POINT('Ctrl Pts',(1.3905130838547,3.34952614641417,1.89579798298361));
#7210=CARTESIAN_POINT('Ctrl Pts',(-2.04523738986722,2.99497715066286,2.05378114823225));
#7211=CARTESIAN_POINT('Ctrl Pts',(-3.62589125240128,-0.0761241329263979,
2.21176431348088));
#7212=CARTESIAN_POINT('Ctrl Pts',(-1.9177361559176,-3.07817520619115,2.36974747872952));
#7213=CARTESIAN_POINT('Ctrl Pts',(1.52987013245233,-3.28821788231848,2.52773064397815));
#7214=CARTESIAN_POINT('Ctrl Pts',(3.58983249342927,-0.515733880008737,2.68571380922678));
#7215=CARTESIAN_POINT('Ctrl Pts',(2.39369399271082,2.72453792342614,2.84369697447542));
#7216=CARTESIAN_POINT('Ctrl Pts',(-0.973606524696896,3.49356106124283,3.00168013972405));
#7217=CARTESIAN_POINT('Ctrl Pts',(-3.45781276429597,1.09380495610431,3.15966330497269));
#7218=CARTESIAN_POINT('Ctrl Pts',(-2.80566476683024,-2.29806951664741,3.31764647022132));
#7219=CARTESIAN_POINT('Ctrl Pts',(0.39131691802336,-3.60551653188198,3.47562963546996));
#7220=CARTESIAN_POINT('Ctrl Pts',(3.23336081192176,-1.64263697190919,3.63361280071859));
#7221=CARTESIAN_POINT('Ctrl Pts',(3.14263608255428,1.81017037953698,3.79159596596722));
#7222=CARTESIAN_POINT('Ctrl Pts',(0.20143316418192,3.62109141633224,3.94957913121586));
#7223=CARTESIAN_POINT('Ctrl Pts',(-2.92247651090087,2.14755894050069,4.1075622964645));
#7224=CARTESIAN_POINT('Ctrl Pts',(-3.39560023944938,-1.27388279388956,4.26554546171314));
#7225=CARTESIAN_POINT('Ctrl Pts',(-0.788798652099944,-3.53986935455429,
4.42352862696176));
#7226=CARTESIAN_POINT('Ctrl Pts',(2.53347023630324,-2.59507358691089,4.5815117922104));
#7227=CARTESIAN_POINT('Ctrl Pts',(3.55779514749501,0.703542499198116,4.73949495745903));
#7228=CARTESIAN_POINT('Ctrl Pts',(1.35507842480211,3.36402152542208,4.89747812270768));
#7229=CARTESIAN_POINT('Ctrl Pts',(-2.07674068097001,2.97321820637517,5.05546128795629));
#7230=CARTESIAN_POINT('Ctrl Pts',(-3.62488510543213,-0.114395507376902,
5.21344445320494));
#7231=CARTESIAN_POINT('Ctrl Pts',(-1.88513501425953,-3.09824859284726,5.37142761845357));
#7232=CARTESIAN_POINT('Ctrl Pts',(1.56449687870927,-3.27188445193808,5.52941078370221));
#7233=CARTESIAN_POINT('Ctrl Pts',(3.59507670274909,-0.477809442042676,5.68739394895084));
#7234=CARTESIAN_POINT('Ctrl Pts',(2.36479925030647,2.74965505068462,5.84537711419948));
#7235=CARTESIAN_POINT('Ctrl Pts',(-1.01043183895086,3.48308854122473,6.00336027944811));
#7236=CARTESIAN_POINT('Ctrl Pts',(-3.469166759934,1.05724187710076,6.16134344469674));
#7237=CARTESIAN_POINT('Ctrl Pts',(-2.78124902365658,-2.32755932727262,6.31932660994538));
#7238=CARTESIAN_POINT('Ctrl Pts',(0.429356514911867,-3.60118463981366,6.47730977519402));
#7239=CARTESIAN_POINT('Ctrl Pts',(3.25052102458439,-1.60841283090018,6.63529294044265));
#7240=CARTESIAN_POINT('Ctrl Pts',(3.12335204644367,1.8432448176368,6.79327610569127));
#7241=CARTESIAN_POINT('Ctrl Pts',(0.163196100475927,3.6230155390935,6.95125927093992));
#7242=CARTESIAN_POINT('Ctrl Pts',(-2.944984173578,2.11658934969185,7.10924243618855));
#7243=CARTESIAN_POINT('Ctrl Pts',(-3.38196348508519,-1.30965915392286,7.26722560143719));
#7244=CARTESIAN_POINT('Ctrl Pts',(-0.751386096246847,-3.5479953461427,7.42520876668581));
#7245=CARTESIAN_POINT('Ctrl Pts',(2.56072339002455,-2.56819159278999,7.58319193193446));
#7246=CARTESIAN_POINT('Ctrl Pts',(3.55017077169744,0.741074350000556,7.74117509718308));
#7247=CARTESIAN_POINT('Ctrl Pts',(1.31948938364505,3.37811317609581,7.89915826243173));
#7248=CARTESIAN_POINT('Ctrl Pts',(-2.10800873502834,2.95117875161517,8.05714142768035));
#7249=CARTESIAN_POINT('Ctrl Pts',(-3.62348089025001,-0.152749143368613,
8.21512459292899));
#7250=CARTESIAN_POINT('Ctrl Pts',(-1.85231323033622,-3.11779603581512,8.37310775817763));
#7251=CARTESIAN_POINT('Ctrl Pts',(1.59892942568934,-3.25553164520284,8.53109092342626));
#7252=CARTESIAN_POINT('Ctrl Pts',(3.59995819558759,-0.439170790472673,8.68907408867489));
#7253=CARTESIAN_POINT('Ctrl Pts',(2.33556733953737,2.77319664798175,8.84705725392354));
#7254=CARTESIAN_POINT('Ctrl Pts',(-1.04699337368903,3.47469407062061,9.00504041917216));
#7255=CARTESIAN_POINT('Ctrl Pts',(-3.48051498243553,1.01550766892132,9.1630235844208));
#7256=CARTESIAN_POINT('Ctrl Pts',(-2.99692813421427,-1.22434708939046,9.26834569458656));
#7257=CARTESIAN_POINT('Ctrl Pts',(-2.33606265769612,-1.99730155693068,9.32100674966943));
#7258=CARTESIAN_POINT('Ctrl Pts',(-0.745932854346924,2.79017756984216,-0.107002249889812));
#7259=CARTESIAN_POINT('Ctrl Pts',(-1.66914448599339,2.5433639279422,-0.0543411948069335));
#7260=CARTESIAN_POINT('Ctrl Pts',(-3.23587888137879,1.06620786278094,0.0509809153588226));
#7261=CARTESIAN_POINT('Ctrl Pts',(-2.66032731473656,-2.13353306696999,0.208964080607457));
#7262=CARTESIAN_POINT('Ctrl Pts',(0.33255207591963,-3.39077348368069,0.366947245856092));
#7263=CARTESIAN_POINT('Ctrl Pts',(3.02160130448948,-1.57610571206399,0.524930411104726));
#7264=CARTESIAN_POINT('Ctrl Pts',(2.97109431199307,1.67002467826918,0.682913576353362));
#7265=CARTESIAN_POINT('Ctrl Pts',(0.225108928408532,3.40040525492435,0.840896741601994));
#7266=CARTESIAN_POINT('Ctrl Pts',(-2.72474746191766,2.04701416957039,0.998879906850632));
#7267=CARTESIAN_POINT('Ctrl Pts',(-3.20332709858383,-1.1633560824147,1.15686307209926));
#7268=CARTESIAN_POINT('Ctrl Pts',(-0.776294983432353,-3.31838293769717,
1.3148462373479));
#7269=CARTESIAN_POINT('Ctrl Pts',(2.3548189081775,-2.46359620146564,1.47282940259653));
#7270=CARTESIAN_POINT('Ctrl Pts',(3.35005480365913,0.625794513789364,1.63081256784517));
#7271=CARTESIAN_POINT('Ctrl Pts',(1.30666456429251,3.14754832119794,1.7887957330938));
#7272=CARTESIAN_POINT('Ctrl Pts',(-1.92190872127375,2.8143787779316,1.94677889834244));
#7273=CARTESIAN_POINT('Ctrl Pts',(-3.40724849589837,-0.0715338159254679,
2.10476206359107));
#7274=CARTESIAN_POINT('Ctrl Pts',(-1.80209586496915,-2.89255995597237,2.26274522883971));
#7275=CARTESIAN_POINT('Ctrl Pts',(1.43761832467147,-3.08993697102635,2.42072839408834));
#7276=CARTESIAN_POINT('Ctrl Pts',(3.37336409514862,-0.484634911700634,2.57871155933697));
#7277=CARTESIAN_POINT('Ctrl Pts',(2.24935324546856,2.56024714901858,2.73669472458561));
#7278=CARTESIAN_POINT('Ctrl Pts',(-0.914897644730358,3.28289787052096,2.89467788983424));
#7279=CARTESIAN_POINT('Ctrl Pts',(-3.24930521080662,1.02784806053531,3.05266105508288));
#7280=CARTESIAN_POINT('Ctrl Pts',(-2.63648200989107,-2.15949496523957,3.21064422033151));
#7281=CARTESIAN_POINT('Ctrl Pts',(0.367720344473012,-3.3881023795338,3.36862738558015));
#7282=CARTESIAN_POINT('Ctrl Pts',(3.03838780488001,-1.54358527662352,3.52661055082878));
#7283=CARTESIAN_POINT('Ctrl Pts',(2.95313381457531,1.70101634981814,3.68459371607742));
#7284=CARTESIAN_POINT('Ctrl Pts',(0.189286660273763,3.40273809194845,3.84257688132605));
#7285=CARTESIAN_POINT('Ctrl Pts',(-2.74624995701975,2.01806023967986,4.00056004657468));
#7286=CARTESIAN_POINT('Ctrl Pts',(-3.19084412718499,-1.19706712951099,4.15854321182332));
#7287=CARTESIAN_POINT('Ctrl Pts',(-0.74123376401713,-3.32641375440981,4.31652637707195));
#7288=CARTESIAN_POINT('Ctrl Pts',(2.38070092320909,-2.43858956605276,4.47450954232059));
#7289=CARTESIAN_POINT('Ctrl Pts',(3.34325861455133,0.661118592733809,4.63249270756923));
#7290=CARTESIAN_POINT('Ctrl Pts',(1.27336662997645,3.16116962279916,4.79047587281786));
#7291=CARTESIAN_POINT('Ctrl Pts',(-1.9515123507689,2.79393190706986,4.94845903806649));
#7292=CARTESIAN_POINT('Ctrl Pts',(-3.40630302001157,-0.107497410516475,
5.10644220331512));
#7293=CARTESIAN_POINT('Ctrl Pts',(-1.7714605857656,-2.91142290903152,5.26442536856377));
#7294=CARTESIAN_POINT('Ctrl Pts',(1.47015706367078,-3.07458845331788,5.42240853381239));
#7295=CARTESIAN_POINT('Ctrl Pts',(3.37829207645675,-0.448997333179196,5.58039169906104));
#7296=CARTESIAN_POINT('Ctrl Pts',(2.22220086809614,2.58384970301577,5.73837486430966));
#7297=CARTESIAN_POINT('Ctrl Pts',(-0.949502377158481,3.27305684783272,5.89635802955831));
#7298=CARTESIAN_POINT('Ctrl Pts',(-3.25997455576684,0.993489750462507,6.05434119480693));
#7299=CARTESIAN_POINT('Ctrl Pts',(-2.61353854622553,-2.18720652797068,6.21232436005557));
#7300=CARTESIAN_POINT('Ctrl Pts',(0.403466137785788,-3.38403170236597,6.3703075253042));
#7301=CARTESIAN_POINT('Ctrl Pts',(3.05451324955387,-1.51142486560757,6.52829069055284));
#7302=CARTESIAN_POINT('Ctrl Pts',(2.93501261389417,1.73209638549038,6.68627385580147));
#7303=CARTESIAN_POINT('Ctrl Pts',(0.153355307475048,3.40454618930379,6.84425702105011));
#7304=CARTESIAN_POINT('Ctrl Pts',(-2.76740039823942,1.98895812812809,7.00224018629874));
#7305=CARTESIAN_POINT('Ctrl Pts',(-3.17802967480296,-1.23068616009594,7.16022335154738));
#7306=CARTESIAN_POINT('Ctrl Pts',(-0.706077200903509,-3.33404974531244,
7.318206516796));
#7307=CARTESIAN_POINT('Ctrl Pts',(2.40631070038151,-2.41332856740186,7.47618968204465));
#7308=CARTESIAN_POINT('Ctrl Pts',(3.33609399179789,0.696387257261517,7.63417284729327));
#7309=CARTESIAN_POINT('Ctrl Pts',(1.23992362286129,3.17441154105332,7.79215601254192));
#7310=CARTESIAN_POINT('Ctrl Pts',(-1.98089492811161,2.77322144063441,7.95013917779054));
#7311=CARTESIAN_POINT('Ctrl Pts',(-3.40498347959126,-0.143538306243407,
8.10812234303918));
#7312=CARTESIAN_POINT('Ctrl Pts',(-1.74061796911753,-2.92979163302642,8.26610550828781));
#7313=CARTESIAN_POINT('Ctrl Pts',(1.50251331369072,-3.05922172765686,8.42408867353645));
#7314=CARTESIAN_POINT('Ctrl Pts',(3.38287921323883,-0.412688608432349,8.58207183878508));
#7315=CARTESIAN_POINT('Ctrl Pts',(2.19473165375214,2.60597173216614,8.74005500403373));
#7316=CARTESIAN_POINT('Ctrl Pts',(-0.983859236085748,3.26516856731113,8.89803816928235));
#7317=CARTESIAN_POINT('Ctrl Pts',(-3.2706384757131,0.954272132462314,9.05602133453099));
#7318=CARTESIAN_POINT('Ctrl Pts',(-2.81621211636024,-1.15051844867672,9.16134344469675));
#7319=CARTESIAN_POINT('Ctrl Pts',(-2.1951971040191,-1.87686343907878,9.21400449977962));
#7320=CARTESIAN_POINT('Ctrl Pts',(-0.698066426161006,2.61113218593862,-0.214004499779622));
#7321=CARTESIAN_POINT('Ctrl Pts',(-1.56203567022649,2.38015654795075,-0.161343444696744));
#7322=CARTESIAN_POINT('Ctrl Pts',(-3.02823289395347,0.997789422974118,-0.0560213345309879));
#7323=CARTESIAN_POINT('Ctrl Pts',(-2.48961440724121,-1.99662448768263,0.101961830717646));
#7324=CARTESIAN_POINT('Ctrl Pts',(0.311212246245525,-3.1731879268769,0.259944995966281));
#7325=CARTESIAN_POINT('Ctrl Pts',(2.8277054853082,-1.47496718405804,0.417928161214915));
#7326=CARTESIAN_POINT('Ctrl Pts',(2.78043952089512,1.56285938066197,0.57591132646355));
#7327=CARTESIAN_POINT('Ctrl Pts',(0.210663713543839,3.18220162843258,0.733894491712185));
#7328=CARTESIAN_POINT('Ctrl Pts',(-2.54990072075242,1.91565749829321,0.891877656960819));
#7329=CARTESIAN_POINT('Ctrl Pts',(-2.99776995543505,-1.08870365217376,1.04986082220945));
#7330=CARTESIAN_POINT('Ctrl Pts',(-0.726480220804574,-3.10544267416671,
1.20784398745809));
#7331=CARTESIAN_POINT('Ctrl Pts',(2.20371044110535,-2.30550750759815,1.36582715270672));
#7332=CARTESIAN_POINT('Ctrl Pts',(3.13508216001732,0.585637349536739,1.52381031795536));
#7333=CARTESIAN_POINT('Ctrl Pts',(1.22281604473031,2.9455704959817,1.68179348320399));
#7334=CARTESIAN_POINT('Ctrl Pts',(-1.79858005268027,2.63378040520035,1.83977664845263));
#7335=CARTESIAN_POINT('Ctrl Pts',(-3.18860573939546,-0.0669434989245405,
1.99775981370126));
#7336=CARTESIAN_POINT('Ctrl Pts',(-1.6864555740207,-2.70694470575358,2.1557429789499));
#7337=CARTESIAN_POINT('Ctrl Pts',(1.3453665168906,-2.89165605973422,2.31372614419853));
#7338=CARTESIAN_POINT('Ctrl Pts',(3.15689569686798,-0.453535943392533,2.47170930944716));
#7339=CARTESIAN_POINT('Ctrl Pts',(2.10501249822631,2.39595637461102,2.6296924746958));
#7340=CARTESIAN_POINT('Ctrl Pts',(-0.856188764763818,3.07223467979908,2.78767563994443));
#7341=CARTESIAN_POINT('Ctrl Pts',(-3.04079765731727,0.961891164966307,2.94565880519307));
#7342=CARTESIAN_POINT('Ctrl Pts',(-2.4672992529519,-2.02092041383173,3.1036419704417));
#7343=CARTESIAN_POINT('Ctrl Pts',(0.344123770922663,-3.17068822718562,3.26162513569034));
#7344=CARTESIAN_POINT('Ctrl Pts',(2.84341479783825,-1.44453358133785,3.41960830093897));
#7345=CARTESIAN_POINT('Ctrl Pts',(2.76363154659633,1.5918623200993,3.5775914661876));
#7346=CARTESIAN_POINT('Ctrl Pts',(0.177140156365606,3.18438476756466,3.73557463143624));
#7347=CARTESIAN_POINT('Ctrl Pts',(-2.57002340313862,1.88856153885904,3.89355779668487));
#7348=CARTESIAN_POINT('Ctrl Pts',(-2.9860880149206,-1.12025146513243,4.05154096193351));
#7349=CARTESIAN_POINT('Ctrl Pts',(-0.693668875934318,-3.11295815426533,
4.20952412718214));
#7350=CARTESIAN_POINT('Ctrl Pts',(2.22793161011494,-2.28210554519462,4.36750729243078));
#7351=CARTESIAN_POINT('Ctrl Pts',(3.12872208160764,0.6186946862695,4.52549045767941));
#7352=CARTESIAN_POINT('Ctrl Pts',(1.1916548351508,2.95831772017624,4.68347362292805));
#7353=CARTESIAN_POINT('Ctrl Pts',(-1.8262840205678,2.61464560776455,4.84145678817668));
#7354=CARTESIAN_POINT('Ctrl Pts',(-3.18772093459101,-0.100599313656048,
4.99943995342532));
#7355=CARTESIAN_POINT('Ctrl Pts',(-1.65778615727167,-2.72459722521578,5.15742311867394));
#7356=CARTESIAN_POINT('Ctrl Pts',(1.3758172486323,-2.87729245469768,5.31540628392259));
#7357=CARTESIAN_POINT('Ctrl Pts',(3.16150745016441,-0.420185224315714,5.47338944917121));
#7358=CARTESIAN_POINT('Ctrl Pts',(2.0796024858858,2.41804435534692,5.63137261441986));
#7359=CARTESIAN_POINT('Ctrl Pts',(-0.888572915366094,3.06302515444072,5.78935577966849));
#7360=CARTESIAN_POINT('Ctrl Pts',(-3.05078235159968,0.929737623824253,5.94733894491712));
#7361=CARTESIAN_POINT('Ctrl Pts',(-2.44582806879447,-2.04685372866874,6.10532211016575));
#7362=CARTESIAN_POINT('Ctrl Pts',(0.377575760659711,-3.16687876491828,6.2633052754144));
#7363=CARTESIAN_POINT('Ctrl Pts',(2.85850547452334,-1.41443690031496,6.42128844066302));
#7364=CARTESIAN_POINT('Ctrl Pts',(2.74667318134467,1.62094795334397,6.57927160591167));
#7365=CARTESIAN_POINT('Ctrl Pts',(0.143514514474167,3.18607683951409,6.73725477116029));
#7366=CARTESIAN_POINT('Ctrl Pts',(-2.58981662290085,1.86132690656433,6.89523793640893));
#7367=CARTESIAN_POINT('Ctrl Pts',(-2.97409586452072,-1.15171316626902,7.05322110165757));
#7368=CARTESIAN_POINT('Ctrl Pts',(-0.660768305560169,-3.12010414448219,
7.2112042669062));
#7369=CARTESIAN_POINT('Ctrl Pts',(2.25189801073846,-2.25846554201373,7.36918743215484));
#7370=CARTESIAN_POINT('Ctrl Pts',(3.12201721189835,0.65170016452248,7.52717059740346));
#7371=CARTESIAN_POINT('Ctrl Pts',(1.16035786207753,2.97070990601083,7.68515376265211));
#7372=CARTESIAN_POINT('Ctrl Pts',(-1.85378112119487,2.59526412965366,7.84313692790074));
#7373=CARTESIAN_POINT('Ctrl Pts',(-3.18648606893251,-0.134327469118203,
8.00112009314937));
#7374=CARTESIAN_POINT('Ctrl Pts',(-1.62892270789884,-2.74178723023772,8.159103258398));
#7375=CARTESIAN_POINT('Ctrl Pts',(1.4060972016921,-2.86291181011087,8.31708642364665));
#7376=CARTESIAN_POINT('Ctrl Pts',(3.16580023089008,-0.386206426392027,8.47506958889527));
#7377=CARTESIAN_POINT('Ctrl Pts',(2.0538959679669,2.43874681635053,8.63305275414391));
#7378=CARTESIAN_POINT('Ctrl Pts',(-0.92072509848246,3.05564306400165,8.79103591939254));
#7379=CARTESIAN_POINT('Ctrl Pts',(-3.06076196899067,0.893036596003309,8.94901908464118));
#7380=CARTESIAN_POINT('Ctrl Pts',(-2.6354960985062,-1.07668980796297,9.05434119480693));
#7381=CARTESIAN_POINT('Ctrl Pts',(-2.05433155034207,-1.75642532122688,9.10700224988981));
#7382=CARTESIAN_POINT('Ctrl Pts',(-0.650199997975088,2.43208680203507,-0.321006749669433));
#7383=CARTESIAN_POINT('Ctrl Pts',(-1.45492685445959,2.21694916795931,-0.268345694586555));
#7384=CARTESIAN_POINT('Ctrl Pts',(-2.82058690652816,0.929370983167296,-0.163023584420799));
#7385=CARTESIAN_POINT('Ctrl Pts',(-2.31890149974585,-1.85971590839527,-0.00504041917216426));
#7386=CARTESIAN_POINT('Ctrl Pts',(0.289872416571416,-2.9556023700731,0.15294274607647));
#7387=CARTESIAN_POINT('Ctrl Pts',(2.63380966612693,-1.37382865605209,0.310925911325105));
#7388=CARTESIAN_POINT('Ctrl Pts',(2.58978472979718,1.45569408305476,0.468909076573739));
#7389=CARTESIAN_POINT('Ctrl Pts',(0.196218498679142,2.96399800194081,0.626892241822374));
#7390=CARTESIAN_POINT('Ctrl Pts',(-2.37505397958718,1.78430082701602,0.784875407071009));
#7391=CARTESIAN_POINT('Ctrl Pts',(-2.79221281228627,-1.01405122193283,0.942858572319641));
#7392=CARTESIAN_POINT('Ctrl Pts',(-0.676665458176792,-2.89250241063626,
1.10084173756828));
#7393=CARTESIAN_POINT('Ctrl Pts',(2.05260197403319,-2.14741881373065,1.25882490281691));
#7394=CARTESIAN_POINT('Ctrl Pts',(2.92010951637551,0.545480185284112,1.41680806806555));
#7395=CARTESIAN_POINT('Ctrl Pts',(1.13896752516812,2.74359267076547,1.57479123331418));
#7396=CARTESIAN_POINT('Ctrl Pts',(-1.67525138408679,2.45318203246909,1.73277439856282));
#7397=CARTESIAN_POINT('Ctrl Pts',(-2.96996298289254,-0.0623531819236091,
1.89075756381145));
#7398=CARTESIAN_POINT('Ctrl Pts',(-1.57081528307225,-2.5213294555348,2.04874072906008));
#7399=CARTESIAN_POINT('Ctrl Pts',(1.25311470910973,-2.6933751484421,2.20672389430872));
#7400=CARTESIAN_POINT('Ctrl Pts',(2.94042729858734,-0.422436975084429,2.36470705955735));
#7401=CARTESIAN_POINT('Ctrl Pts',(1.96067175098405,2.23166560020346,2.52269022480599));
#7402=CARTESIAN_POINT('Ctrl Pts',(-0.797479884797277,2.86157148907721,2.68067339005462));
#7403=CARTESIAN_POINT('Ctrl Pts',(-2.83229010382792,0.895934269397302,2.83865655530326));
#7404=CARTESIAN_POINT('Ctrl Pts',(-2.29811649601273,-1.8823458624239,2.99663972055189));
#7405=CARTESIAN_POINT('Ctrl Pts',(0.320527197372314,-2.95327407483744,3.15462288580053));
#7406=CARTESIAN_POINT('Ctrl Pts',(2.6484417907965,-1.34548188605218,3.31260605104916));
#7407=CARTESIAN_POINT('Ctrl Pts',(2.57412927861735,1.48270829038046,3.47058921629779));
#7408=CARTESIAN_POINT('Ctrl Pts',(0.164993652457452,2.96603144318087,3.62857238154644));
#7409=CARTESIAN_POINT('Ctrl Pts',(-2.3937968492575,1.75906283803822,3.78655554679506));
#7410=CARTESIAN_POINT('Ctrl Pts',(-2.7813319026562,-1.04343580075386,3.94453871204371));
#7411=CARTESIAN_POINT('Ctrl Pts',(-0.646103987851508,-2.89950255412085,
4.10252187729233));
#7412=CARTESIAN_POINT('Ctrl Pts',(2.07516229702079,-2.12562152433648,4.26050504254097));
#7413=CARTESIAN_POINT('Ctrl Pts',(2.91418554866396,0.576270779805192,4.41848820778961));
#7414=CARTESIAN_POINT('Ctrl Pts',(1.10994304032514,2.75546581755331,4.57647137303824));
#7415=CARTESIAN_POINT('Ctrl Pts',(-1.70105569036669,2.43535930845924,4.73445453828687));
#7416=CARTESIAN_POINT('Ctrl Pts',(-2.96913884917045,-0.0937012167956214,
4.8924377035355));
#7417=CARTESIAN_POINT('Ctrl Pts',(-1.54411172877774,-2.53777154140003,5.05042086878415));
#7418=CARTESIAN_POINT('Ctrl Pts',(1.28147743359381,-2.67999645607747,5.20840403403276));
#7419=CARTESIAN_POINT('Ctrl Pts',(2.94472282387208,-0.391373115452234,5.36638719928142));
#7420=CARTESIAN_POINT('Ctrl Pts',(1.93700410367547,2.25223900767807,5.52437036453004));
#7421=CARTESIAN_POINT('Ctrl Pts',(-0.827643453573711,2.85299346104872,5.68235352977868));
#7422=CARTESIAN_POINT('Ctrl Pts',(-2.84159014743252,0.865985497185999,5.84033669502731));
#7423=CARTESIAN_POINT('Ctrl Pts',(-2.27811759136341,-1.90650092936679,5.99831986027594));
#7424=CARTESIAN_POINT('Ctrl Pts',(0.351685383533634,-2.9497258274706,6.15630302552458));
#7425=CARTESIAN_POINT('Ctrl Pts',(2.66249769949282,-1.31744893502235,6.31428619077321));
#7426=CARTESIAN_POINT('Ctrl Pts',(2.55833374879516,1.50979952119754,6.47226935602186));
#7427=CARTESIAN_POINT('Ctrl Pts',(0.133673721473288,2.96760748972438,6.63025252127048));
#7428=CARTESIAN_POINT('Ctrl Pts',(-2.41223284756227,1.73369568500057,6.78823568651912));
#7429=CARTESIAN_POINT('Ctrl Pts',(-2.77016205423848,-1.07274017244211,6.94621885176775));
#7430=CARTESIAN_POINT('Ctrl Pts',(-0.615459410216834,-2.90615854365194,
7.10420201701639));
#7431=CARTESIAN_POINT('Ctrl Pts',(2.09748532109543,-2.10360251662561,7.26218518226503));
#7432=CARTESIAN_POINT('Ctrl Pts',(2.9079404319988,0.60701307178344,7.42016834751365));
#7433=CARTESIAN_POINT('Ctrl Pts',(1.08079210129377,2.76700827096834,7.5781515127623));
#7434=CARTESIAN_POINT('Ctrl Pts',(-1.72666731427814,2.41730681867291,7.73613467801093));
#7435=CARTESIAN_POINT('Ctrl Pts',(-2.96798865827376,-0.125116631992998,
7.89411784325956));
#7436=CARTESIAN_POINT('Ctrl Pts',(-1.51722744668015,-2.55378282744902,8.05210100850819));
#7437=CARTESIAN_POINT('Ctrl Pts',(1.30968108969348,-2.66660189256488,8.21008417375684));
#7438=CARTESIAN_POINT('Ctrl Pts',(2.94872124854132,-0.359724244351702,8.36806733900546));
#7439=CARTESIAN_POINT('Ctrl Pts',(1.91306028218166,2.27152190053491,8.52605050425411));
#7440=CARTESIAN_POINT('Ctrl Pts',(-0.857590960879173,2.84611756069217,8.68403366950273));
#7441=CARTESIAN_POINT('Ctrl Pts',(-2.85088546226824,0.831801059544302,8.84201683475137));
#7442=CARTESIAN_POINT('Ctrl Pts',(-2.45478008065217,-1.00286116724922,8.94733894491712));
#7443=CARTESIAN_POINT('Ctrl Pts',(-1.91346599666504,-1.63598720337498,9.));
#7444=CARTESIAN_POINT('Ctrl Pts',(-1.91346599666504,-1.63598720337498,9.));
#7445=CARTESIAN_POINT('Ctrl Pts',(-1.97510122930192,-1.57806521937354,9.));
#7446=CARTESIAN_POINT('Ctrl Pts',(-2.03336858029506,-1.51699427545506,9.));
#7447=CARTESIAN_POINT('Ctrl Pts',(-2.08826957682143,-1.45315876516108,9.));
#7448=CARTESIAN_POINT('Ctrl Pts',(-2.14462126052521,-1.38763648482453,9.));
#7449=CARTESIAN_POINT('Ctrl Pts',(-2.1974267747986,-1.31920117573619,9.));
#7450=CARTESIAN_POINT('Ctrl Pts',(-2.24666228537762,-1.24821996122214,9.));
#7451=CARTESIAN_POINT('Ctrl Pts',(-2.29723808834736,-1.17530649129776,9.));
#7452=CARTESIAN_POINT('Ctrl Pts',(-2.34404740976649,-1.09970606249909,9.));
#7453=CARTESIAN_POINT('Ctrl Pts',(-2.38703036306917,-1.02177364893372,9.));
#7454=CARTESIAN_POINT('Ctrl Pts',(-2.4059069163696,-0.987548560952,9.));
#7455=CARTESIAN_POINT('Ctrl Pts',(-2.42404501517521,-0.95287321932183,9.));
#7456=CARTESIAN_POINT('Ctrl Pts',(-2.4414371795908,-0.917775628914927,9.));
#7457=CARTESIAN_POINT('Ctrl Pts',(-2.45136171608851,-0.897747798643102,
9.));
#7458=CARTESIAN_POINT('Ctrl Pts',(-2.4610433321017,-0.877582454455379,9.));
#7459=CARTESIAN_POINT('Ctrl Pts',(-2.47048040473327,-0.857284652451543,
9.));
#7460=CARTESIAN_POINT('Ctrl Pts',(-2.4790010742832,-0.838957903234229,9.));
#7461=CARTESIAN_POINT('Ctrl Pts',(-2.48732477223045,-0.820517427059542,
9.));
#7462=CARTESIAN_POINT('Ctrl Pts',(-2.49543660387403,-0.801998763017973,
9.));
#7463=CARTESIAN_POINT('Ctrl Pts',(-2.53203081792429,-0.718457093807081,
9.));
#7464=CARTESIAN_POINT('Ctrl Pts',(-2.56436348011502,-0.63323212592296,9.));
#7465=CARTESIAN_POINT('Ctrl Pts',(-2.5924085980561,-0.546721977487591,9.));
#7466=CARTESIAN_POINT('Ctrl Pts',(-2.62091304129589,-0.458794958570371,
9.));
#7467=CARTESIAN_POINT('Ctrl Pts',(-2.64498884113912,-0.369539561869024,
9.));
#7468=CARTESIAN_POINT('Ctrl Pts',(-2.66456964086263,-0.279336683014174,
9.));
#7469=CARTESIAN_POINT('Ctrl Pts',(-2.68356521302629,-0.191829772221376,
9.));
#7470=CARTESIAN_POINT('Ctrl Pts',(-2.69833062202798,-0.10343025333291,9.));
#7471=CARTESIAN_POINT('Ctrl Pts',(-2.70876448070549,-0.0144639948968432,
9.));
#7472=CARTESIAN_POINT('Ctrl Pts',(-2.71312791197798,0.0227416225314671,
9.));
#7473=CARTESIAN_POINT('Ctrl Pts',(-2.71673328148375,0.0600465487674368,
9.));
#7474=CARTESIAN_POINT('Ctrl Pts',(-2.71957085608624,0.09742756389295,9.));
#7475=CARTESIAN_POINT('Ctrl Pts',(-2.72134533161258,0.120803758630415,9.));
#7476=CARTESIAN_POINT('Ctrl Pts',(-2.72281952388506,0.144209714226741,9.));
#7477=CARTESIAN_POINT('Ctrl Pts',(-2.72399076243517,0.167639784643834,9.));
#7478=CARTESIAN_POINT('Ctrl Pts',(-2.72467743928119,0.181376428519216,9.));
#7479=CARTESIAN_POINT('Ctrl Pts',(-2.72525970776296,0.19511678651136,9.00000000000001));
#7480=CARTESIAN_POINT('Ctrl Pts',(-2.72573704181005,0.208851493316018,9.00000000000001));
#7481=CARTESIAN_POINT('Ctrl Pts',(-2.72911014315679,0.305908383145141,9.00000000000001));
#7482=CARTESIAN_POINT('Ctrl Pts',(-2.72725356321717,0.402803406061901,9.));
#7483=CARTESIAN_POINT('Ctrl Pts',(-2.7201015526238,0.499115315406068,9.));
#7484=CARTESIAN_POINT('Ctrl Pts',(-2.71294954203042,0.595427224750235,9.));
#7485=CARTESIAN_POINT('Ctrl Pts',(-2.70050253761008,0.69115707285682,9.));
#7486=CARTESIAN_POINT('Ctrl Pts',(-2.68264189514795,0.785902555476956,9.));
#7487=CARTESIAN_POINT('Ctrl Pts',(-2.6655684581099,0.876472143641819,9.));
#7488=CARTESIAN_POINT('Ctrl Pts',(-2.64354819167242,0.966143195066629,9.));
#7489=CARTESIAN_POINT('Ctrl Pts',(-2.61685636836744,1.05467578508374,9.));
#7490=CARTESIAN_POINT('Ctrl Pts',(-2.60792497911495,1.08429980191986,9.));
#7491=CARTESIAN_POINT('Ctrl Pts',(-2.59847010448723,1.11379631508768,9.));
#7492=CARTESIAN_POINT('Ctrl Pts',(-2.58850078352238,1.14315615835076,9.));
#7493=CARTESIAN_POINT('Ctrl Pts',(-2.58205201908924,1.16214789446448,9.));
#7494=CARTESIAN_POINT('Ctrl Pts',(-2.57538798275344,1.18108244148084,9.));
#7495=CARTESIAN_POINT('Ctrl Pts',(-2.56851098701296,1.19995728413151,9.));
#7496=CARTESIAN_POINT('Ctrl Pts',(-2.56187356995564,1.21817457076241,9.));
#7497=CARTESIAN_POINT('Ctrl Pts',(-2.55503596749083,1.23634058633936,9.));
#7498=CARTESIAN_POINT('Ctrl Pts',(-2.5480112160171,1.25442550206745,9.));
#7499=CARTESIAN_POINT('Ctrl Pts',(-2.51416429529988,1.34156292053919,9.));
#7500=CARTESIAN_POINT('Ctrl Pts',(-2.47593826775787,1.42692993566585,9.00000000000001));
#7501=CARTESIAN_POINT('Ctrl Pts',(-2.43366482457034,1.51029236193381,9.00000000000001));
#7502=CARTESIAN_POINT('Ctrl Pts',(-2.38981580722589,1.59676179048456,9.00000000000001));
#7503=CARTESIAN_POINT('Ctrl Pts',(-2.34161192708367,1.68107514437489,9.));
#7504=CARTESIAN_POINT('Ctrl Pts',(-2.28936736609892,1.76296811103273,9.));
#7505=CARTESIAN_POINT('Ctrl Pts',(-2.23652986509351,1.84579050682973,9.));
#7506=CARTESIAN_POINT('Ctrl Pts',(-2.1795590352686,1.92613808521401,9.));
#7507=CARTESIAN_POINT('Ctrl Pts',(-2.11872806710601,2.00372262354843,9.));
#7508=CARTESIAN_POINT('Ctrl Pts',(-2.07707869447161,2.0568427274258,9.));
#7509=CARTESIAN_POINT('Ctrl Pts',(-2.0336186907015,2.10866727264771,9.));
#7510=CARTESIAN_POINT('Ctrl Pts',(-1.98842354991113,2.15909672967731,9.));
#7511=CARTESIAN_POINT('Ctrl Pts',(-1.97696960898531,2.17187721916438,9.));
#7512=CARTESIAN_POINT('Ctrl Pts',(-1.96540269677891,2.1845695710529,9.));
#7513=CARTESIAN_POINT('Ctrl Pts',(-1.95373641455615,2.1971589298009,9.));
#7514=CARTESIAN_POINT('Ctrl Pts',(-1.88513603210895,2.27118721133798,9.));
#7515=CARTESIAN_POINT('Ctrl Pts',(-1.81301936191858,2.34175191206966,8.99999999999999));
#7516=CARTESIAN_POINT('Ctrl Pts',(-1.73769803691675,2.4085627715844,9.));
#7517=CARTESIAN_POINT('Ctrl Pts',(-1.67462788387254,2.46450670425561,9.));
#7518=CARTESIAN_POINT('Ctrl Pts',(-1.60930970274182,2.51781862546635,9.));
#7519=CARTESIAN_POINT('Ctrl Pts',(-1.54190247847365,2.56831427040715,9.));
#7520=CARTESIAN_POINT('Ctrl Pts',(-1.50803174514331,2.59368728558025,9.));
#7521=CARTESIAN_POINT('Ctrl Pts',(-1.47363323977049,2.61834899713265,9.));
#7522=CARTESIAN_POINT('Ctrl Pts',(-1.43872534941306,2.64227437840376,9.));
#7523=CARTESIAN_POINT('Ctrl Pts',(-1.42333762902739,2.65282090737903,9.));
#7524=CARTESIAN_POINT('Ctrl Pts',(-1.40785862868675,2.66321904138253,9.));
#7525=CARTESIAN_POINT('Ctrl Pts',(-1.39229155460026,2.67346610734178,9.));
#7526=CARTESIAN_POINT('Ctrl Pts',(-1.30709673728478,2.72954581169518,9.));
#7527=CARTESIAN_POINT('Ctrl Pts',(-1.21925453406997,2.78111212367673,9.));
#7528=CARTESIAN_POINT('Ctrl Pts',(-1.12905379957436,2.82785493889709,9.));
#7529=CARTESIAN_POINT('Ctrl Pts',(-1.04989418514209,2.86887614843616,9.));
#7530=CARTESIAN_POINT('Ctrl Pts',(-0.968917198642337,2.90618241367003,9.));
#7531=CARTESIAN_POINT('Ctrl Pts',(-0.886295500097728,2.93953989917748,9.));
#7532=CARTESIAN_POINT('Ctrl Pts',(-0.856268073332328,2.95166310011376,9.));
#7533=CARTESIAN_POINT('Ctrl Pts',(-0.826023230498369,2.96326448152923,9.));
#7534=CARTESIAN_POINT('Ctrl Pts',(-0.795573338178555,2.97434764200039,9.));
#7535=CARTESIAN_POINT('Ctrl Pts',(-2.52134266056864,-0.000655147898209446,
7.88741669750802));
#7536=CARTESIAN_POINT('Ctrl Pts',(-2.52146223070113,-0.0358370156486364,
7.88965041275853));
#7537=CARTESIAN_POINT('Ctrl Pts',(-2.52078886170416,-0.0710141084424755,
7.89188412800905));
#7538=CARTESIAN_POINT('Ctrl Pts',(-2.51930823234222,-0.106157089457993,
7.89411784325956));
#7539=CARTESIAN_POINT('Ctrl Pts',(-2.48440158774256,-0.93467203047832,7.94677889834244));
#7540=CARTESIAN_POINT('Ctrl Pts',(-2.00081451721136,-1.74422742896367,7.99943995342531));
#7541=CARTESIAN_POINT('Ctrl Pts',(-1.28786955921681,-2.16780830572565,8.05210100850819));
#7542=CARTESIAN_POINT('Ctrl Pts',(-0.574924601222266,-2.59138918248764,
8.10476206359107));
#7543=CARTESIAN_POINT('Ctrl Pts',(0.367378244235608,-2.62899553752626,8.15742311867395));
#7544=CARTESIAN_POINT('Ctrl Pts',(1.11170302677253,-2.26331910701003,8.21008417375683));
#7545=CARTESIAN_POINT('Ctrl Pts',(1.85602780930943,-1.89764267649381,8.26274522883971));
#7546=CARTESIAN_POINT('Ctrl Pts',(2.40237452892538,-1.12868346042275,8.31540628392258));
#7547=CARTESIAN_POINT('Ctrl Pts',(2.50293772767341,-0.305662828239462,8.36806733900546));
#7548=CARTESIAN_POINT('Ctrl Pts',(2.60350092642144,0.517357803943831,8.42072839408834));
#7549=CARTESIAN_POINT('Ctrl Pts',(2.25828060430155,1.39443985223937,8.47338944917123));
#7550=CARTESIAN_POINT('Ctrl Pts',(1.62389523606481,1.92874681974668,8.5260505042541));
#7551=CARTESIAN_POINT('Ctrl Pts',(0.989509867828049,2.463053787254,8.57871155933698));
#7552=CARTESIAN_POINT('Ctrl Pts',(0.0659594534744365,2.65458567397309,8.63137261441985));
#7553=CARTESIAN_POINT('Ctrl Pts',(-0.72803150393389,2.41463220047464,8.68403366950273));
#7554=CARTESIAN_POINT('Ctrl Pts',(-1.5220224613422,2.17467872697621,8.73669472458561));
#7555=CARTESIAN_POINT('Ctrl Pts',(-2.18645396180522,1.50323989326025,8.78935577966849));
#7556=CARTESIAN_POINT('Ctrl Pts',(-2.41964336663271,0.708854919703897,8.84201683475137));
#7557=CARTESIAN_POINT('Ctrl Pts',(-2.48665536097282,0.480571300252128,8.85715012233692));
#7558=CARTESIAN_POINT('Ctrl Pts',(-2.51805435150169,0.242134494478738,8.87228340992247));
#7559=CARTESIAN_POINT('Ctrl Pts',(-2.51592828109546,0.00320694493696498,
8.88741669750802));
#7560=CARTESIAN_POINT('Ctrl Pts',(-0.793799282532843,2.9692229537457,-1.11022302462516E-15));
#7561=CARTESIAN_POINT('Ctrl Pts',(-0.886878369010734,2.93517420813052,-1.08381449128764E-15));
#7562=CARTESIAN_POINT('Ctrl Pts',(-0.977892018175826,2.89636073172584,-1.25693831090626E-15));
#7563=CARTESIAN_POINT('Ctrl Pts',(-1.06663133989414,2.85310975855297,-1.32185928869433E-15));
#7564=CARTESIAN_POINT('Ctrl Pts',(-1.15732372244669,2.80890687612374,-1.38820911016277E-15));
#7565=CARTESIAN_POINT('Ctrl Pts',(-1.24564123287364,2.76006840206767,-1.51535923310734E-15));
#7566=CARTESIAN_POINT('Ctrl Pts',(-1.3313319520912,2.70689814245137,-1.60982338570648E-15));
#7567=CARTESIAN_POINT('Ctrl Pts',(-1.41378112297932,2.65573923211314,-1.70071410446299E-15));
#7568=CARTESIAN_POINT('Ctrl Pts',(-1.49379876348973,2.6005691930734,-9.63096719719295E-16));
#7569=CARTESIAN_POINT('Ctrl Pts',(-1.57112748186993,2.54162859144216,-9.08995101411847E-16));
#7570=CARTESIAN_POINT('Ctrl Pts',(-1.63879011045261,2.49005556501483,-8.6165618539283E-16));
#7571=CARTESIAN_POINT('Ctrl Pts',(-1.70439374270875,2.43559500480107,-1.16765261517047E-15));
#7572=CARTESIAN_POINT('Ctrl Pts',(-1.76774130072772,2.3783953552462,-1.12410081243297E-15));
#7573=CARTESIAN_POINT('Ctrl Pts',(-1.78181886636062,2.36568402357109,-1.11442240681417E-15));
#7574=CARTESIAN_POINT('Ctrl Pts',(-1.79578759750834,2.35283474575188,-1.12368001218868E-15));
#7575=CARTESIAN_POINT('Ctrl Pts',(-1.80962592284842,2.33986750951544,-1.12410081243297E-15));
#7576=CARTESIAN_POINT('Ctrl Pts',(-1.88206109072238,2.27199196023008,-1.12630344429686E-15));
#7577=CARTESIAN_POINT('Ctrl Pts',(-1.95103069838081,2.20079578495377,-1.65761929008765E-15));
#7578=CARTESIAN_POINT('Ctrl Pts',(-2.01629458396089,2.12656832619519,-1.59594559789866E-15));
#7579=CARTESIAN_POINT('Ctrl Pts',(-2.08119360973793,2.05275583837715,-1.53461669442375E-15));
#7580=CARTESIAN_POINT('Ctrl Pts',(-2.14242871756392,1.97594507073483,-1.54117032658774E-15));
#7581=CARTESIAN_POINT('Ctrl Pts',(-2.19972015237435,1.89639377131377,-1.55431223447522E-15));
#7582=CARTESIAN_POINT('Ctrl Pts',(-2.25491823235702,1.81974917334377,-1.56697395406905E-15));
#7583=CARTESIAN_POINT('Ctrl Pts',(-2.30645573607158,1.74055992058549,-1.37357914314464E-15));
#7584=CARTESIAN_POINT('Ctrl Pts',(-2.35403753012578,1.65904287815286,-1.346145417358E-15));
#7585=CARTESIAN_POINT('Ctrl Pts',(-2.37402503340242,1.62480032414432,-1.3346214364962E-15));
#7586=CARTESIAN_POINT('Ctrl Pts',(-2.39331395745324,1.59014691080251,-8.58817840424498E-16));
#7587=CARTESIAN_POINT('Ctrl Pts',(-2.4118798230075,1.55509841026105,-8.32667268468867E-16));
#7588=CARTESIAN_POINT('Ctrl Pts',(-2.42490921652519,1.53050161974646,-8.1431498148677E-16));
#7589=CARTESIAN_POINT('Ctrl Pts',(-2.43758246139463,1.50571024066321,-9.02295645932798E-16));
#7590=CARTESIAN_POINT('Ctrl Pts',(-2.44989061107463,1.4807297179593,-8.74300631892311E-16));
#7591=CARTESIAN_POINT('Ctrl Pts',(-2.45765251973512,1.46497620987237,-8.56646090179653E-16));
#7592=CARTESIAN_POINT('Ctrl Pts',(-2.46527012151294,1.44914532838183,-1.01327467154504E-15));
#7593=CARTESIAN_POINT('Ctrl Pts',(-2.47273147665068,1.4332596231852,-1.01307850997046E-15));
#7594=CARTESIAN_POINT('Ctrl Pts',(-2.51485688189898,1.34357192481016,-1.01197101868087E-15));
#7595=CARTESIAN_POINT('Ctrl Pts',(-2.55207895507421,1.25199537848123,-1.57756955155647E-15));
#7596=CARTESIAN_POINT('Ctrl Pts',(-2.58410579009646,1.15880114788537,-1.55431223447522E-15));
#7597=CARTESIAN_POINT('Ctrl Pts',(-2.61396690786283,1.07190889352943,-1.53262762268606E-15));
#7598=CARTESIAN_POINT('Ctrl Pts',(-2.63931147777468,0.98360954884976,-7.90704564077518E-16));
#7599=CARTESIAN_POINT('Ctrl Pts',(-2.65985235348906,0.894114165208975,-7.49400541621981E-16));
#7600=CARTESIAN_POINT('Ctrl Pts',(-2.66134210780213,0.887623393557723,-7.46404912494191E-16));
#7601=CARTESIAN_POINT('Ctrl Pts',(-2.66280657151596,0.881126329458841,-1.17195010629658E-15));
#7602=CARTESIAN_POINT('Ctrl Pts',(-2.66424562422382,0.874623053092889,-1.16573417585641E-15));
#7603=CARTESIAN_POINT('Ctrl Pts',(-2.68482996036177,0.781599617617434,-1.04692289900001E-15));
#7604=CARTESIAN_POINT('Ctrl Pts',(-2.70021925475279,0.687304125014347,-9.81473364557526E-16));
#7605=CARTESIAN_POINT('Ctrl Pts',(-2.71049072825162,0.592145729463149,-8.60422844084496E-16));
#7606=CARTESIAN_POINT('Ctrl Pts',(-2.71630566600268,0.538274184481477,-7.91893120343947E-16));
#7607=CARTESIAN_POINT('Ctrl Pts',(-2.72047941991799,0.484126269723892,-1.33893866460458E-15));
#7608=CARTESIAN_POINT('Ctrl Pts',(-2.72301911106579,0.429778916423232,-1.33226762955019E-15));
#7609=CARTESIAN_POINT('Ctrl Pts',(-2.72366582651429,0.415939724600469,-1.330568894871E-15));
#7610=CARTESIAN_POINT('Ctrl Pts',(-2.72420643309896,0.402088998021608,-1.4283520817037E-15));
#7611=CARTESIAN_POINT('Ctrl Pts',(-2.72464086766462,0.388240253329536,-1.41553435639707E-15));
#7612=CARTESIAN_POINT('Ctrl Pts',(-2.72756562491765,0.295005921429125,-1.32924118817005E-15));
#7613=CARTESIAN_POINT('Ctrl Pts',(-2.72569020906838,0.201710259987124,-1.06406896392454E-15));
#7614=CARTESIAN_POINT('Ctrl Pts',(-2.71914970277427,0.108729654609856,-1.0547118733939E-15));
#7615=CARTESIAN_POINT('Ctrl Pts',(-2.71259881332269,0.0156014410469117,
-1.04533992833364E-15));
#7616=CARTESIAN_POINT('Ctrl Pts',(-2.7013676305465,-0.0772116972142303,
-1.39298541692603E-15));
#7617=CARTESIAN_POINT('Ctrl Pts',(-2.68554097073859,-0.169319449958644,
-1.38777878078145E-15));
#7618=CARTESIAN_POINT('Ctrl Pts',(-2.66994267605977,-0.260098166816704,
-1.38264727193154E-15));
#7619=CARTESIAN_POINT('Ctrl Pts',(-2.64988010285609,-0.35019255259287,-1.0308343657274E-15));
#7620=CARTESIAN_POINT('Ctrl Pts',(-2.62539147593809,-0.439203699437016,
-8.88178419700125E-16));
#7621=CARTESIAN_POINT('Ctrl Pts',(-2.61615129561636,-0.472789863750656,
-8.34350711447145E-16));
#7622=CARTESIAN_POINT('Ctrl Pts',(-2.60628055155745,-0.506221478197271,
-1.63486821342447E-15));
#7623=CARTESIAN_POINT('Ctrl Pts',(-2.59577987598867,-0.539475785607662,
-1.63757896132211E-15));
#7624=CARTESIAN_POINT('Ctrl Pts',(-2.58810257712511,-0.563788817166238,
-1.63956085492672E-15));
#7625=CARTESIAN_POINT('Ctrl Pts',(-2.58008853706366,-0.588007054833637,
-1.58037810929509E-15));
#7626=CARTESIAN_POINT('Ctrl Pts',(-2.57173775820317,-0.612121310772716,
-1.60982338570648E-15));
#7627=CARTESIAN_POINT('Ctrl Pts',(-2.56654706379232,-0.627110299897659,
-1.62812604157221E-15));
#7628=CARTESIAN_POINT('Ctrl Pts',(-2.5612292056814,-0.642050561982069,-1.68622661660371E-15));
#7629=CARTESIAN_POINT('Ctrl Pts',(-2.55578549619449,-0.656937632559102,
-1.69309011255336E-15));
#7630=CARTESIAN_POINT('Ctrl Pts',(-2.52407271214207,-0.743663504966145,
-1.73307398116711E-15));
#7631=CARTESIAN_POINT('Ctrl Pts',(-2.48808276034648,-0.828614815980182,
-9.77241205803787E-16));
#7632=CARTESIAN_POINT('Ctrl Pts',(-2.44787616909233,-0.911389584879519,
-1.22124532708767E-15));
#7633=CARTESIAN_POINT('Ctrl Pts',(-2.41772122565171,-0.973470661554021,
-1.40424841805059E-15));
#7634=CARTESIAN_POINT('Ctrl Pts',(-2.38519343314366,-1.03432694837566,-1.06885018652311E-15));
#7635=CARTESIAN_POINT('Ctrl Pts',(-2.35030323620402,-1.09377384664802,-1.16573417585641E-15));
#7636=CARTESIAN_POINT('Ctrl Pts',(-2.33453826171165,-1.12063465332491,-1.20951075938217E-15));
#7637=CARTESIAN_POINT('Ctrl Pts',(-2.31829080415985,-1.14720751443845,-1.51219465577998E-15));
#7638=CARTESIAN_POINT('Ctrl Pts',(-2.3015610494714,-1.17347433375359,-1.60982338570648E-15));
#7639=CARTESIAN_POINT('Ctrl Pts',(-2.2924218706108,-1.18782344790922,-1.66315629114043E-15));
#7640=CARTESIAN_POINT('Ctrl Pts',(-2.28314390690011,-1.20207312067747,-1.37933724003994E-15));
#7641=CARTESIAN_POINT('Ctrl Pts',(-2.27372792141341,-1.21622019271053,-1.33226762955019E-15));
#7642=CARTESIAN_POINT('Ctrl Pts',(-2.2261576244293,-1.2876923098902,-1.09446826663856E-15));
#7643=CARTESIAN_POINT('Ctrl Pts',(-2.17506395390716,-1.35655363510998,-6.67815194483028E-16));
#7644=CARTESIAN_POINT('Ctrl Pts',(-2.1204781354577,-1.42244994398426,-2.77555756156289E-16));
#7645=CARTESIAN_POINT('Ctrl Pts',(-2.07432924150386,-1.47816114987198,5.23841796256794E-17));
#7646=CARTESIAN_POINT('Ctrl Pts',(-2.02568360871182,-1.53175271241673,-1.28432281748436E-16));
#7647=CARTESIAN_POINT('Ctrl Pts',(-1.97454380027699,-1.58298639353747,-1.66533453693773E-16));
#7648=CARTESIAN_POINT('Ctrl Pts',(-1.9557112793937,-1.60185348356312,-6.86465273718822E-17));
#7649=CARTESIAN_POINT('Ctrl Pts',(-1.93654037332315,-1.62040056709866,1.19381178188368E-16));
#7650=CARTESIAN_POINT('Ctrl Pts',(-1.91704123069774,-1.63862336360398,1.11022302462516E-16));
#7651=CARTESIAN_POINT('Origin',(0.,0.,9.));
#7652=CARTESIAN_POINT('',(-7.,-8.57252759403147E-16,9.));
#7653=CARTESIAN_POINT('Origin',(0.,0.,9.));
#7654=CARTESIAN_POINT('Origin',(0.,0.,4.));
#7655=CARTESIAN_POINT('',(-7.,-8.57252759403147E-16,4.));
#7656=CARTESIAN_POINT('Origin',(0.,0.,4.));
#7657=CARTESIAN_POINT('',(-5.,-6.12323399573677E-16,4.));
#7658=CARTESIAN_POINT('Origin',(0.,0.,4.));
#7659=CARTESIAN_POINT('Origin',(0.,0.,2.));
#7660=CARTESIAN_POINT('',(-7.,-8.57252759403147E-16,2.));
#7661=CARTESIAN_POINT('Origin',(0.,0.,2.));
#7662=CARTESIAN_POINT('',(-5.,6.12323399573677E-16,2.));
#7663=CARTESIAN_POINT('Origin',(0.,0.,2.));
#7664=CARTESIAN_POINT('Origin',(0.,0.,2.));
#7665=CARTESIAN_POINT('',(-7.,-8.57252759403147E-16,2.));
#7666=CARTESIAN_POINT('Origin',(0.,0.,0.));
#7667=CARTESIAN_POINT('',(-5.,-6.12323399573677E-16,0.));
#7668=CARTESIAN_POINT('',(-5.,-6.12323399573677E-16,0.));
#7669=CARTESIAN_POINT('Origin',(0.,0.,0.));
#7670=CARTESIAN_POINT('Origin',(0.,0.,8.));
#7671=CARTESIAN_POINT('',(-7.,-8.57252759403147E-16,8.));
#7672=CARTESIAN_POINT('Origin',(0.,0.,8.));
#7673=CARTESIAN_POINT('',(-5.,-6.12323399573677E-16,8.));
#7674=CARTESIAN_POINT('Origin',(0.,0.,8.));
#7675=CARTESIAN_POINT('Origin',(0.,0.,8.));
#7676=CARTESIAN_POINT('',(-7.,-8.57252759403147E-16,8.));
#7677=CARTESIAN_POINT('Origin',(0.,0.,0.));
#7678=CARTESIAN_POINT('Origin',(0.,0.,0.));
#7679=CARTESIAN_POINT('',(-5.,-6.12323399573677E-16,0.));
#7680=CARTESIAN_POINT('Origin',(0.,0.,0.));
#9762=UNCERTAINTY_MEASURE_WITH_UNIT(LENGTH_MEASURE(0.01),#9778,
'DISTANCE_ACCURACY_VALUE',
'Maximum model space distance between geometric entities at asserted c
onnectivities');
#9764=UNCERTAINTY_MEASURE_WITH_UNIT(LENGTH_MEASURE(0.01),#9778,
'DISTANCE_ACCURACY_VALUE',
'Maximum model space distance between geometric entities at asserted c
onnectivities');
#9775=(
GEOMETRIC_REPRESENTATION_CONTEXT(3)
GLOBAL_UNCERTAINTY_ASSIGNED_CONTEXT((#9762))
GLOBAL_UNIT_ASSIGNED_CONTEXT((#9778,#9780,#9781))
REPRESENTATION_CONTEXT('','3D')
);
#9777=(
GEOMETRIC_REPRESENTATION_CONTEXT(3)
GLOBAL_UNCERTAINTY_ASSIGNED_CONTEXT((#9764))
GLOBAL_UNIT_ASSIGNED_CONTEXT((#9778,#9780,#9781))
REPRESENTATION_CONTEXT('','3D')
);
#9778=(
LENGTH_UNIT()
NAMED_UNIT(*)
SI_UNIT(.MILLI.,.METRE.)
);
#9780=(
NAMED_UNIT(*)
PLANE_ANGLE_UNIT()
SI_UNIT($,.RADIAN.)
);
#9781=(
NAMED_UNIT(*)
SI_UNIT($,.STERADIAN.)
SOLID_ANGLE_UNIT()
);
#9792=SHAPE_DEFINITION_REPRESENTATION(#9804,#9866);
#9804=PRODUCT_DEFINITION_SHAPE('',$,#9879);
#9866=SHAPE_REPRESENTATION('',(#4216),#9775);
#9868=PRODUCT_DEFINITION_CONTEXT('part definition',#9906,'design');
#9879=PRODUCT_DEFINITION('Rivet nut M6','Rivet nut M6',#9891,#9868);
#9891=PRODUCT_DEFINITION_FORMATION('',$,#9918);
#9906=APPLICATION_CONTEXT(
'Core Data for Automotive Mechanical Design Process');
#9907=PRODUCT_CONTEXT('part definition',#9906,'mechanical');
#9918=PRODUCT('Rivet nut M6','Rivet nut M6',$,(#9907));
#9929=PRESENTATION_STYLE_ASSIGNMENT((#9940));
#9940=SURFACE_STYLE_USAGE(.BOTH.,#9951);
#9951=SURFACE_SIDE_STYLE('',(#9962));
#9962=SURFACE_STYLE_FILL_AREA(#9973);
#9973=FILL_AREA_STYLE('Nut gray',(#9984));
#9984=FILL_AREA_STYLE_COLOUR('Nut gray',#9995);
#9995=COLOUR_RGB('Nut gray',0.407843137254902,0.447058823529412,0.498039215686275);
ENDSEC;
END-ISO-10303-21;
